ISO-10303-21;
HEADER;
/* Generated by software containing ST-Developer
 * from STEP Tools, Inc. (www.steptools.com) 
 */
/* OPTION: using custom renumber hook */

FILE_DESCRIPTION(
/* description */ ('STEP AP242 Edition 2', 'CAx-IF Rec.Pracs.---Representation and Presentation of Product Manufa
cturing Information (PMI)---4.0---2014-10-13', 'CAx-IF Rec.Pracs.---3D Tessellated Geometry---0.4---2014-09-14', '2;1', 'CAx-IF Rec.Pracs.---User Defined Attributes---1.5---2016-08-15'),
/* implementation_level */ '2;1');

FILE_NAME(
/* name */ 'CRANKSHAFT.step',
/* time_stamp */ '2026-10-07T00:00:55Z',
/* author */ (''),
/* organization */ (''),
/* preprocessor_version */ 'ST-DEVELOPER v20',
/* originating_system */ 'ONSHAPE BY PTC INC, 1.221',
/* authorisation */ '  ');

FILE_SCHEMA (('AP242_MANAGED_MODEL_BASED_3D_ENGINEERING_MIM_LF { 1 0 10303 442 3 1 4 }'));
ENDSEC;

DATA;
#45=ELLIPSE('',#4974,0.0243340224134753,0.023999999999999);
#46=ELLIPSE('',#4977,0.0243340224134761,0.024000000000001);
#47=ELLIPSE('',#4992,0.00666547755067305,0.00299999999999906);
#48=ELLIPSE('',#4993,0.0127089644991076,0.00300000000000008);
#49=ELLIPSE('',#4995,0.0132410741485331,0.00299999999999985);
#50=ELLIPSE('',#5007,0.00308724563751592,0.003);
#51=ELLIPSE('',#5008,0.0127089644991094,0.00300000000000053);
#52=ELLIPSE('',#5009,0.00308724563751592,0.003);
#53=ELLIPSE('',#5015,0.00308009663615096,0.003);
#54=ELLIPSE('',#5024,0.00653928253453561,0.003);
#55=ELLIPSE('',#5027,0.0243340224134758,0.0240000000000003);
#56=ELLIPSE('',#5030,0.0243340224134756,0.0239999999999998);
#126=SHAPE_REPRESENTATION_RELATIONSHIP('','',#4482,#137);
#137=ADVANCED_BREP_SHAPE_REPRESENTATION('',(#4458),#8545);
#200=CONICAL_SURFACE('',#4988,0.001,1.05851587994953);
#201=CONICAL_SURFACE('',#4989,0.001,1.05851587994953);
#202=CONICAL_SURFACE('',#5040,0.001,1.05851587994953);
#203=CONICAL_SURFACE('',#5044,0.001,1.05851587994953);
#281=CYLINDRICAL_SURFACE('',#4961,0.023455);
#282=CYLINDRICAL_SURFACE('',#4968,0.023455);
#283=CYLINDRICAL_SURFACE('',#4975,0.025);
#284=CYLINDRICAL_SURFACE('',#4979,0.023);
#285=CYLINDRICAL_SURFACE('',#4982,0.024);
#286=CYLINDRICAL_SURFACE('',#4987,0.005);
#287=CYLINDRICAL_SURFACE('',#4990,0.005);
#288=CYLINDRICAL_SURFACE('',#4991,0.003);
#289=CYLINDRICAL_SURFACE('',#4994,0.003);
#290=CYLINDRICAL_SURFACE('',#4996,0.04);
#291=CYLINDRICAL_SURFACE('',#4997,0.031);
#292=CYLINDRICAL_SURFACE('',#4999,0.029);
#293=CYLINDRICAL_SURFACE('',#5006,0.003);
#294=CYLINDRICAL_SURFACE('',#5010,0.029);
#295=CYLINDRICAL_SURFACE('',#5014,0.003);
#296=CYLINDRICAL_SURFACE('',#5021,0.003);
#297=CYLINDRICAL_SURFACE('',#5022,0.003);
#298=CYLINDRICAL_SURFACE('',#5023,0.003);
#299=CYLINDRICAL_SURFACE('',#5025,0.003);
#300=CYLINDRICAL_SURFACE('',#5028,0.025);
#301=CYLINDRICAL_SURFACE('',#5032,0.031);
#302=CYLINDRICAL_SURFACE('',#5034,0.024);
#303=CYLINDRICAL_SURFACE('',#5039,0.005);
#304=CYLINDRICAL_SURFACE('',#5045,0.005);
#305=CYLINDRICAL_SURFACE('',#5046,0.04);
#548=CIRCLE('',#4962,0.023455);
#549=CIRCLE('',#4963,0.023455);
#550=CIRCLE('',#4965,0.031);
#551=CIRCLE('',#4966,0.0316935480501236);
#552=CIRCLE('',#4967,0.031693548050133);
#553=CIRCLE('',#4969,0.023455);
#554=CIRCLE('',#4970,0.023455);
#555=CIRCLE('',#4972,0.025);
#556=CIRCLE('',#4980,0.023);
#557=CIRCLE('',#4981,0.023);
#558=CIRCLE('',#4984,0.00499999999999991);
#559=CIRCLE('',#4985,0.04);
#560=CIRCLE('',#4986,0.005);
#561=CIRCLE('',#4998,0.031);
#562=CIRCLE('',#5000,0.029);
#563=CIRCLE('',#5001,0.029);
#564=CIRCLE('',#5002,0.00298497776938405);
#565=CIRCLE('',#5003,0.00298497542639763);
#566=CIRCLE('',#5004,0.00298498584851454);
#567=CIRCLE('',#5005,0.00298498508188116);
#568=CIRCLE('',#5011,0.029);
#569=CIRCLE('',#5012,0.029);
#570=CIRCLE('',#5013,0.00298508178884043);
#571=CIRCLE('',#5018,0.025);
#572=CIRCLE('',#5020,0.031);
#573=CIRCLE('',#5033,0.031);
#574=CIRCLE('',#5036,0.00499999999999984);
#575=CIRCLE('',#5037,0.04);
#576=CIRCLE('',#5038,0.0049999999999997);
#577=CIRCLE('',#5041,0.0316935480501328);
#578=CIRCLE('',#5043,0.0316935480501328);
#673=B_SPLINE_CURVE_WITH_KNOTS('',3,(#8104,#8105,#8106,#8107,#8108,#8109),
 .UNSPECIFIED.,.F.,.F.,(4,1,1,4),(-0.0376586249368312,-0.0177089806563706,
-0.00773415851614028,0.00224066362409002),.UNSPECIFIED.);
#674=B_SPLINE_CURVE_WITH_KNOTS('',3,(#8110,#8111,#8112,#8113,#8114,#8115),
 .UNSPECIFIED.,.F.,.F.,(4,1,1,4),(4.39785759961698E-16,0.0187757639234785,
0.0281636458852176,0.0375515278469566),.UNSPECIFIED.);
#675=B_SPLINE_CURVE_WITH_KNOTS('',3,(#8126,#8127,#8128,#8129,#8130,#8131,
#8132,#8133,#8134,#8135,#8136,#8137,#8138,#8139,#8140,#8141,#8142,#8143,
#8144,#8145,#8146,#8147),.UNSPECIFIED.,.F.,.F.,(4,1,1,1,1,1,1,1,1,1,1,1,
1,1,1,1,1,1,1,4),(0.,0.00451289465242826,0.00902578930485651,0.0135386839572848,
0.018051578609713,0.0203080259359271,0.0225644732621413,0.0270773679145695,
0.0293338152407837,0.0315902625669978,0.0338467098932119,0.036103157219426,
0.0406160518718543,0.0451289465242826,0.0496418411767108,0.0541547358291391,
0.0586676304815673,0.0631805251339956,0.0676934197864238,0.0722063144388521),
 .UNSPECIFIED.);
#676=B_SPLINE_CURVE_WITH_KNOTS('',3,(#8149,#8150,#8151,#8152,#8153,#8154),
 .UNSPECIFIED.,.F.,.F.,(4,1,1,4),(4.14598910758457E-16,0.00990633188871804,
0.0198126637774357,0.0396253275548709),.UNSPECIFIED.);
#677=B_SPLINE_CURVE_WITH_KNOTS('',3,(#8163,#8164,#8165,#8166,#8167),
 .UNSPECIFIED.,.F.,.F.,(4,1,4),(7.75791922889773E-18,0.0187679100601147,
0.0375358201202294),.UNSPECIFIED.);
#678=B_SPLINE_CURVE_WITH_KNOTS('',3,(#8171,#8172,#8173,#8174,#8175,#8176,
#8177,#8178,#8179),.UNSPECIFIED.,.F.,.F.,(4,1,1,1,1,1,4),(0.,0.00246792104240225,
0.00370188156360338,0.0049358420848045,0.00616980260600563,0.00740376312720676,
0.00987168416960901),.UNSPECIFIED.);
#679=B_SPLINE_CURVE_WITH_KNOTS('',3,(#8182,#8183,#8184,#8185,#8186,#8187,
#8188,#8189,#8190),.UNSPECIFIED.,.F.,.F.,(4,1,1,1,1,1,4),(4.03187682893047E-19,
0.00253597196642849,0.00380395794964274,0.00507194393285698,0.00633992991607123,
0.00760791589928547,0.010143887865714),.UNSPECIFIED.);
#680=B_SPLINE_CURVE_WITH_KNOTS('',3,(#8204,#8205,#8206,#8207),
 .UNSPECIFIED.,.F.,.F.,(4,4),(2.1900902092527E-7,0.0027185779941561),
 .UNSPECIFIED.);
#681=B_SPLINE_CURVE_WITH_KNOTS('',3,(#8211,#8212,#8213,#8214,#8215,#8216,
#8217,#8218,#8219,#8220,#8221,#8222,#8223,#8224,#8225,#8226,#8227,#8228,
#8229,#8230,#8231,#8232),.UNSPECIFIED.,.F.,.F.,(4,1,1,1,1,1,1,1,1,1,1,1,
1,1,1,1,1,1,1,4),(2.15427911492917E-7,0.00612092101240522,0.0122416265968989,
0.0183623321813927,0.0244830377658864,0.0306037433503801,0.0367244489348739,
0.0397848017271207,0.0428451545193676,0.0489658601038613,0.0520262128961082,
0.055086565688355,0.0612072712728488,0.0673279768573425,0.0703883296495894,
0.0734486824418362,0.0795693880263299,0.0856900936108237,0.0918107991953174,
0.0979315047798111),.UNSPECIFIED.);
#682=B_SPLINE_CURVE_WITH_KNOTS('',3,(#8234,#8235,#8236,#8237),
 .UNSPECIFIED.,.F.,.F.,(4,4),(2.15328326043877E-7,0.00271635611451793),
 .UNSPECIFIED.);
#683=B_SPLINE_CURVE_WITH_KNOTS('',3,(#8246,#8247,#8248,#8249,#8250,#8251,
#8252,#8253,#8254),.UNSPECIFIED.,.F.,.F.,(4,1,1,1,1,1,4),(0.,0.00248512918851248,
0.00372769378276871,0.00497025837702495,0.00621282297128119,0.00745538756553743,
0.0099405167540499),.UNSPECIFIED.);
#684=B_SPLINE_CURVE_WITH_KNOTS('',3,(#8259,#8260,#8261,#8262,#8263,#8264,
#8265,#8266,#8267),.UNSPECIFIED.,.F.,.F.,(4,1,1,1,1,1,4),(0.,0.00247246452692368,
0.00370869679038551,0.00494492905384735,0.00618116131730919,0.00741739358077102,
0.0098898581076947),.UNSPECIFIED.);
#685=B_SPLINE_CURVE_WITH_KNOTS('',3,(#8281,#8282,#8283,#8284,#8285,#8286,
#8287,#8288,#8289),.UNSPECIFIED.,.F.,.F.,(4,1,1,1,1,1,4),(4.33680868994202E-19,
0.00217116695540332,0.00325675043310498,0.00434233391080664,0.00542791738850829,
0.00651350086620995,0.00868466782161327),.UNSPECIFIED.);
#686=B_SPLINE_CURVE_WITH_KNOTS('',3,(#8293,#8294,#8295,#8296,#8297,#8298,
#8299,#8300,#8301),.UNSPECIFIED.,.F.,.F.,(4,1,1,1,1,1,4),(1.98874244301294E-16,
0.00217116695540802,0.00325675043311192,0.00434233391081583,0.00542791738851974,
0.00651350086622365,0.00868466782163146),.UNSPECIFIED.);
#687=B_SPLINE_CURVE_WITH_KNOTS('',3,(#8305,#8306,#8307,#8308,#8309,#8310,
#8311,#8312,#8313),.UNSPECIFIED.,.F.,.F.,(4,1,1,1,1,1,4),(2.94857387122129E-16,
0.00248512918850741,0.00372769378276096,0.00497025837701452,0.00621282297126808,
0.00745538756552163,0.00994051675402874),.UNSPECIFIED.);
#688=B_SPLINE_CURVE_WITH_KNOTS('',3,(#8323,#8324,#8325,#8326),
 .UNSPECIFIED.,.F.,.F.,(4,4),(0.,0.000678185781570246),.UNSPECIFIED.);
#689=B_SPLINE_CURVE_WITH_KNOTS('',3,(#8330,#8331,#8332,#8333,#8334,#8335,
#8336,#8337,#8338),.UNSPECIFIED.,.F.,.F.,(4,1,1,1,1,1,4),(7.152448122691E-18,
0.00214700943930209,0.00322051415895314,0.00429401887860418,0.00536752359825522,
0.00644102831790627,0.00858803775720835),.UNSPECIFIED.);
#690=B_SPLINE_CURVE_WITH_KNOTS('',3,(#8339,#8340,#8341,#8342,#8343,#8344,
#8345,#8346,#8347,#8348,#8349),.UNSPECIFIED.,.T.,.F.,(1,1,1,1,1,1,1,1,1,
1,1,1,1,1,1),(-0.00703767296465454,-0.00469178197643636,-0.00234589098821818,
0.,0.00234589098821818,0.00469178197643636,0.00703767296465454,0.00938356395287272,
0.0117294549410909,0.0140753459293091,0.0164212369175273,0.0187671279057454,
0.0211130188939636,0.0234589098821818,0.0258048008704),.UNSPECIFIED.);
#691=B_SPLINE_CURVE_WITH_KNOTS('',3,(#8381,#8382,#8383,#8384,#8385,#8386),
 .UNSPECIFIED.,.F.,.F.,(4,1,1,4),(4.30194153152991E-16,0.0195333936657401,
0.0293000904986099,0.0390667873314798),.UNSPECIFIED.);
#692=B_SPLINE_CURVE_WITH_KNOTS('',3,(#8390,#8391,#8392,#8393,#8394),
 .UNSPECIFIED.,.F.,.F.,(4,1,4),(1.16627099047498E-16,0.0187679100601151,
0.03753582012023),.UNSPECIFIED.);
#693=B_SPLINE_CURVE_WITH_KNOTS('',3,(#8401,#8402,#8403,#8404,#8405,#8406,
#8407,#8408,#8409,#8410,#8411,#8412,#8413,#8414,#8415,#8416,#8417,#8418,
#8419,#8420,#8421,#8422),.UNSPECIFIED.,.F.,.F.,(4,1,1,1,1,1,1,1,1,1,1,1,
1,1,1,1,1,1,1,4),(1.02803407384313E-16,0.00451289465242834,0.00902578930485658,
0.0135386839572848,0.0180515786097131,0.0203080259359272,0.0225644732621413,
0.0270773679145695,0.0293338152407837,0.0315902625669978,0.0338467098932119,
0.036103157219426,0.0406160518718543,0.0451289465242825,0.0496418411767107,
0.054154735829139,0.0586676304815672,0.0631805251339955,0.0676934197864237,
0.0722063144388519),.UNSPECIFIED.);
#694=B_SPLINE_CURVE_WITH_KNOTS('',3,(#8424,#8425,#8426,#8427,#8428,#8429),
 .UNSPECIFIED.,.F.,.F.,(4,1,1,4),(2.19892879980849E-16,0.018775763923479,
0.0281636458852184,0.0375515278469578),.UNSPECIFIED.);
#695=B_SPLINE_CURVE_WITH_KNOTS('',3,(#8433,#8434,#8435,#8436,#8437),
 .UNSPECIFIED.,.F.,.F.,(4,1,4),(0.,0.0195237738539724,0.0390475477079449),
 .UNSPECIFIED.);
#696=B_SPLINE_CURVE_WITH_KNOTS('',3,(#8462,#8463,#8464,#8465),
 .UNSPECIFIED.,.F.,.F.,(4,4),(4.39402408874622E-16,0.00271835452853781),
 .UNSPECIFIED.);
#697=B_SPLINE_CURVE_WITH_KNOTS('',3,(#8468,#8469,#8470,#8471,#8472,#8473,
#8474,#8475,#8476,#8477,#8478,#8479,#8480,#8481,#8482,#8483,#8484,#8485,
#8486,#8487,#8488,#8489),.UNSPECIFIED.,.F.,.F.,(4,1,1,1,1,1,1,1,1,1,1,1,
1,1,1,1,1,1,1,4),(2.52579550652517E-17,0.00612070517530055,0.0122414103506011,
0.0183621155259016,0.0244828207012021,0.0306035258765026,0.0367242310518032,
0.0397845836394534,0.0428449362271037,0.0489656414024042,0.0520259939900545,
0.0550863465777047,0.0612070517530053,0.0673277569283058,0.070388109515956,
0.0734484621036063,0.0795691672789068,0.0856898724542074,0.0918105776295079,
0.0979312828048084),.UNSPECIFIED.);
#698=B_SPLINE_CURVE_WITH_KNOTS('',3,(#8491,#8492,#8493,#8494),
 .UNSPECIFIED.,.F.,.F.,(4,4),(0.,0.00271613773257923),.UNSPECIFIED.);
#1635=ORIENTED_EDGE('',*,*,#2337,.T.);
#1636=ORIENTED_EDGE('',*,*,#2338,.F.);
#1637=ORIENTED_EDGE('',*,*,#2339,.T.);
#1638=ORIENTED_EDGE('',*,*,#2340,.T.);
#1639=ORIENTED_EDGE('',*,*,#2341,.F.);
#1640=ORIENTED_EDGE('',*,*,#2342,.T.);
#1641=ORIENTED_EDGE('',*,*,#2343,.F.);
#1642=ORIENTED_EDGE('',*,*,#2344,.T.);
#1643=ORIENTED_EDGE('',*,*,#2345,.F.);
#1644=ORIENTED_EDGE('',*,*,#2346,.F.);
#1645=ORIENTED_EDGE('',*,*,#2347,.F.);
#1646=ORIENTED_EDGE('',*,*,#2348,.F.);
#1647=ORIENTED_EDGE('',*,*,#2349,.F.);
#1648=ORIENTED_EDGE('',*,*,#2345,.T.);
#1649=ORIENTED_EDGE('',*,*,#2350,.F.);
#1650=ORIENTED_EDGE('',*,*,#2351,.F.);
#1651=ORIENTED_EDGE('',*,*,#2352,.T.);
#1652=ORIENTED_EDGE('',*,*,#2340,.F.);
#1653=ORIENTED_EDGE('',*,*,#2353,.T.);
#1654=ORIENTED_EDGE('',*,*,#2354,.F.);
#1655=ORIENTED_EDGE('',*,*,#2346,.T.);
#1656=ORIENTED_EDGE('',*,*,#2355,.T.);
#1657=ORIENTED_EDGE('',*,*,#2356,.T.);
#1658=ORIENTED_EDGE('',*,*,#2357,.T.);
#1659=ORIENTED_EDGE('',*,*,#2358,.F.);
#1660=ORIENTED_EDGE('',*,*,#2347,.T.);
#1661=ORIENTED_EDGE('',*,*,#2354,.T.);
#1662=ORIENTED_EDGE('',*,*,#2359,.F.);
#1663=ORIENTED_EDGE('',*,*,#2360,.T.);
#1664=ORIENTED_EDGE('',*,*,#2361,.T.);
#1665=ORIENTED_EDGE('',*,*,#2362,.T.);
#1666=ORIENTED_EDGE('',*,*,#2363,.F.);
#1667=ORIENTED_EDGE('',*,*,#2364,.F.);
#1668=ORIENTED_EDGE('',*,*,#2348,.T.);
#1669=ORIENTED_EDGE('',*,*,#2358,.T.);
#1670=ORIENTED_EDGE('',*,*,#2365,.T.);
#1671=ORIENTED_EDGE('',*,*,#2342,.F.);
#1672=ORIENTED_EDGE('',*,*,#2350,.T.);
#1673=ORIENTED_EDGE('',*,*,#2349,.T.);
#1674=ORIENTED_EDGE('',*,*,#2364,.T.);
#1675=ORIENTED_EDGE('',*,*,#2366,.F.);
#1676=ORIENTED_EDGE('',*,*,#2355,.F.);
#1677=ORIENTED_EDGE('',*,*,#2367,.T.);
#1678=ORIENTED_EDGE('',*,*,#2368,.T.);
#1679=ORIENTED_EDGE('',*,*,#2369,.T.);
#1680=ORIENTED_EDGE('',*,*,#2370,.F.);
#1681=ORIENTED_EDGE('',*,*,#2363,.T.);
#1682=ORIENTED_EDGE('',*,*,#2371,.F.);
#1683=ORIENTED_EDGE('',*,*,#2356,.F.);
#1684=ORIENTED_EDGE('',*,*,#2366,.T.);
#1685=ORIENTED_EDGE('',*,*,#2362,.F.);
#1686=ORIENTED_EDGE('',*,*,#2372,.T.);
#1687=ORIENTED_EDGE('',*,*,#2373,.F.);
#1688=ORIENTED_EDGE('',*,*,#2374,.T.);
#1689=ORIENTED_EDGE('',*,*,#2357,.F.);
#1690=ORIENTED_EDGE('',*,*,#2371,.T.);
#1691=ORIENTED_EDGE('',*,*,#2375,.F.);
#1692=ORIENTED_EDGE('',*,*,#2351,.T.);
#1693=ORIENTED_EDGE('',*,*,#2374,.F.);
#1694=ORIENTED_EDGE('',*,*,#2376,.F.);
#1695=ORIENTED_EDGE('',*,*,#2352,.F.);
#1696=ORIENTED_EDGE('',*,*,#2375,.T.);
#1697=ORIENTED_EDGE('',*,*,#2377,.T.);
#1698=ORIENTED_EDGE('',*,*,#2378,.T.);
#1699=ORIENTED_EDGE('',*,*,#2360,.F.);
#1700=ORIENTED_EDGE('',*,*,#2341,.T.);
#1701=ORIENTED_EDGE('',*,*,#2365,.F.);
#1702=ORIENTED_EDGE('',*,*,#2359,.T.);
#1703=ORIENTED_EDGE('',*,*,#2353,.F.);
#1704=ORIENTED_EDGE('',*,*,#2343,.T.);
#1705=ORIENTED_EDGE('',*,*,#2378,.F.);
#1706=ORIENTED_EDGE('',*,*,#2379,.T.);
#1707=ORIENTED_EDGE('',*,*,#2372,.F.);
#1708=ORIENTED_EDGE('',*,*,#2361,.F.);
#1709=ORIENTED_EDGE('',*,*,#2380,.F.);
#1710=ORIENTED_EDGE('',*,*,#2367,.F.);
#1711=ORIENTED_EDGE('',*,*,#2381,.T.);
#1712=ORIENTED_EDGE('',*,*,#2382,.F.);
#1713=ORIENTED_EDGE('',*,*,#2368,.F.);
#1714=ORIENTED_EDGE('',*,*,#2380,.T.);
#1715=ORIENTED_EDGE('',*,*,#2383,.F.);
#1716=ORIENTED_EDGE('',*,*,#2384,.F.);
#1717=ORIENTED_EDGE('',*,*,#2377,.F.);
#1718=ORIENTED_EDGE('',*,*,#2376,.T.);
#1719=ORIENTED_EDGE('',*,*,#2373,.T.);
#1720=ORIENTED_EDGE('',*,*,#2379,.F.);
#1721=ORIENTED_EDGE('',*,*,#2385,.F.);
#1722=ORIENTED_EDGE('',*,*,#2339,.F.);
#1723=ORIENTED_EDGE('',*,*,#2386,.F.);
#1724=ORIENTED_EDGE('',*,*,#2387,.F.);
#1725=ORIENTED_EDGE('',*,*,#2388,.T.);
#1726=ORIENTED_EDGE('',*,*,#2382,.T.);
#1727=ORIENTED_EDGE('',*,*,#2389,.T.);
#1728=ORIENTED_EDGE('',*,*,#2390,.T.);
#1729=ORIENTED_EDGE('',*,*,#2391,.T.);
#1730=ORIENTED_EDGE('',*,*,#2392,.T.);
#1731=ORIENTED_EDGE('',*,*,#2393,.T.);
#1732=ORIENTED_EDGE('',*,*,#2394,.T.);
#1733=ORIENTED_EDGE('',*,*,#2395,.T.);
#1734=ORIENTED_EDGE('',*,*,#2391,.F.);
#1735=ORIENTED_EDGE('',*,*,#2396,.T.);
#1736=ORIENTED_EDGE('',*,*,#2393,.F.);
#1737=ORIENTED_EDGE('',*,*,#2389,.F.);
#1738=ORIENTED_EDGE('',*,*,#2381,.F.);
#1739=ORIENTED_EDGE('',*,*,#2388,.F.);
#1740=ORIENTED_EDGE('',*,*,#2397,.F.);
#1741=ORIENTED_EDGE('',*,*,#2398,.F.);
#1742=ORIENTED_EDGE('',*,*,#2399,.F.);
#1743=ORIENTED_EDGE('',*,*,#2400,.T.);
#1744=ORIENTED_EDGE('',*,*,#2384,.T.);
#1745=ORIENTED_EDGE('',*,*,#2401,.T.);
#1746=ORIENTED_EDGE('',*,*,#2402,.T.);
#1747=ORIENTED_EDGE('',*,*,#2403,.T.);
#1748=ORIENTED_EDGE('',*,*,#2403,.F.);
#1749=ORIENTED_EDGE('',*,*,#2404,.T.);
#1750=ORIENTED_EDGE('',*,*,#2401,.F.);
#1751=ORIENTED_EDGE('',*,*,#2383,.T.);
#1752=ORIENTED_EDGE('',*,*,#2400,.F.);
#1753=ORIENTED_EDGE('',*,*,#2399,.T.);
#1754=ORIENTED_EDGE('',*,*,#2385,.T.);
#1755=ORIENTED_EDGE('',*,*,#2405,.T.);
#1756=ORIENTED_EDGE('',*,*,#2406,.F.);
#1757=ORIENTED_EDGE('',*,*,#2407,.T.);
#1758=ORIENTED_EDGE('',*,*,#2408,.F.);
#1759=ORIENTED_EDGE('',*,*,#2337,.F.);
#1760=ORIENTED_EDGE('',*,*,#2409,.F.);
#1761=ORIENTED_EDGE('',*,*,#2387,.T.);
#1762=ORIENTED_EDGE('',*,*,#2410,.F.);
#1763=ORIENTED_EDGE('',*,*,#2397,.T.);
#1764=ORIENTED_EDGE('',*,*,#2390,.F.);
#1765=ORIENTED_EDGE('',*,*,#2392,.F.);
#1766=ORIENTED_EDGE('',*,*,#2395,.F.);
#1767=ORIENTED_EDGE('',*,*,#2411,.T.);
#1768=ORIENTED_EDGE('',*,*,#2396,.F.);
#1769=ORIENTED_EDGE('',*,*,#2394,.F.);
#1770=ORIENTED_EDGE('',*,*,#2402,.F.);
#1771=ORIENTED_EDGE('',*,*,#2404,.F.);
#1772=ORIENTED_EDGE('',*,*,#2412,.F.);
#1773=ORIENTED_EDGE('',*,*,#2413,.F.);
#1774=ORIENTED_EDGE('',*,*,#2414,.F.);
#1775=ORIENTED_EDGE('',*,*,#2415,.F.);
#1776=ORIENTED_EDGE('',*,*,#2416,.F.);
#1777=ORIENTED_EDGE('',*,*,#2417,.F.);
#1778=ORIENTED_EDGE('',*,*,#2418,.F.);
#1779=ORIENTED_EDGE('',*,*,#2405,.F.);
#1780=ORIENTED_EDGE('',*,*,#2419,.F.);
#1781=ORIENTED_EDGE('',*,*,#2420,.F.);
#1782=ORIENTED_EDGE('',*,*,#2406,.T.);
#1783=ORIENTED_EDGE('',*,*,#2418,.T.);
#1784=ORIENTED_EDGE('',*,*,#2421,.T.);
#1785=ORIENTED_EDGE('',*,*,#2407,.F.);
#1786=ORIENTED_EDGE('',*,*,#2420,.T.);
#1787=ORIENTED_EDGE('',*,*,#2422,.F.);
#1788=ORIENTED_EDGE('',*,*,#2423,.F.);
#1789=ORIENTED_EDGE('',*,*,#2424,.F.);
#1790=ORIENTED_EDGE('',*,*,#2425,.T.);
#1791=ORIENTED_EDGE('',*,*,#2426,.F.);
#1792=ORIENTED_EDGE('',*,*,#2427,.T.);
#1793=ORIENTED_EDGE('',*,*,#2428,.T.);
#1794=ORIENTED_EDGE('',*,*,#2409,.T.);
#1795=ORIENTED_EDGE('',*,*,#2408,.T.);
#1796=ORIENTED_EDGE('',*,*,#2428,.F.);
#1797=ORIENTED_EDGE('',*,*,#2429,.T.);
#1798=ORIENTED_EDGE('',*,*,#2419,.T.);
#1799=ORIENTED_EDGE('',*,*,#2430,.T.);
#1800=ORIENTED_EDGE('',*,*,#2410,.T.);
#1801=ORIENTED_EDGE('',*,*,#2427,.F.);
#1802=ORIENTED_EDGE('',*,*,#2431,.T.);
#1803=ORIENTED_EDGE('',*,*,#2412,.T.);
#1804=ORIENTED_EDGE('',*,*,#2429,.F.);
#1805=ORIENTED_EDGE('',*,*,#2426,.T.);
#1806=ORIENTED_EDGE('',*,*,#2432,.T.);
#1807=ORIENTED_EDGE('',*,*,#2433,.F.);
#1808=ORIENTED_EDGE('',*,*,#2434,.T.);
#1809=ORIENTED_EDGE('',*,*,#2413,.T.);
#1810=ORIENTED_EDGE('',*,*,#2431,.F.);
#1811=ORIENTED_EDGE('',*,*,#2435,.F.);
#1812=ORIENTED_EDGE('',*,*,#2436,.F.);
#1813=ORIENTED_EDGE('',*,*,#2414,.T.);
#1814=ORIENTED_EDGE('',*,*,#2434,.F.);
#1815=ORIENTED_EDGE('',*,*,#2424,.T.);
#1816=ORIENTED_EDGE('',*,*,#2437,.F.);
#1817=ORIENTED_EDGE('',*,*,#2415,.T.);
#1818=ORIENTED_EDGE('',*,*,#2436,.T.);
#1819=ORIENTED_EDGE('',*,*,#2438,.F.);
#1820=ORIENTED_EDGE('',*,*,#2439,.T.);
#1821=ORIENTED_EDGE('',*,*,#2430,.F.);
#1822=ORIENTED_EDGE('',*,*,#2416,.T.);
#1823=ORIENTED_EDGE('',*,*,#2437,.T.);
#1824=ORIENTED_EDGE('',*,*,#2423,.T.);
#1825=ORIENTED_EDGE('',*,*,#2440,.T.);
#1826=ORIENTED_EDGE('',*,*,#2417,.T.);
#1827=ORIENTED_EDGE('',*,*,#2440,.F.);
#1828=ORIENTED_EDGE('',*,*,#2422,.T.);
#1829=ORIENTED_EDGE('',*,*,#2421,.F.);
#1830=ORIENTED_EDGE('',*,*,#2425,.F.);
#1831=ORIENTED_EDGE('',*,*,#2439,.F.);
#1832=ORIENTED_EDGE('',*,*,#2441,.T.);
#1833=ORIENTED_EDGE('',*,*,#2432,.F.);
#1834=ORIENTED_EDGE('',*,*,#2438,.T.);
#1835=ORIENTED_EDGE('',*,*,#2435,.T.);
#1836=ORIENTED_EDGE('',*,*,#2433,.T.);
#1837=ORIENTED_EDGE('',*,*,#2441,.F.);
#1838=ORIENTED_EDGE('',*,*,#2386,.T.);
#1839=ORIENTED_EDGE('',*,*,#2411,.F.);
#1840=ORIENTED_EDGE('',*,*,#2398,.T.);
#1841=ORIENTED_EDGE('',*,*,#2369,.F.);
#1842=ORIENTED_EDGE('',*,*,#2338,.T.);
#1843=ORIENTED_EDGE('',*,*,#2370,.T.);
#1844=ORIENTED_EDGE('',*,*,#2344,.F.);
#2337=EDGE_CURVE('',#2752,#2752,#548,.T.);
#2338=EDGE_CURVE('',#2753,#2753,#549,.T.);
#2339=EDGE_CURVE('',#2754,#2754,#550,.T.);
#2340=EDGE_CURVE('',#2755,#2756,#2968,.T.);
#2341=EDGE_CURVE('',#2757,#2756,#551,.T.);
#2342=EDGE_CURVE('',#2757,#2758,#2969,.T.);
#2343=EDGE_CURVE('',#2755,#2758,#552,.T.);
#2344=EDGE_CURVE('',#2759,#2759,#553,.T.);
#2345=EDGE_CURVE('',#2760,#2760,#554,.T.);
#2346=EDGE_CURVE('',#2761,#2762,#2970,.T.);
#2347=EDGE_CURVE('',#2763,#2761,#555,.T.);
#2348=EDGE_CURVE('',#2764,#2763,#2971,.T.);
#2349=EDGE_CURVE('',#2760,#2764,#2972,.T.);
#2350=EDGE_CURVE('',#2762,#2760,#2973,.T.);
#2351=EDGE_CURVE('',#2765,#2766,#2974,.T.);
#2352=EDGE_CURVE('',#2765,#2756,#673,.T.);
#2353=EDGE_CURVE('',#2755,#2767,#674,.T.);
#2354=EDGE_CURVE('',#2761,#2767,#2975,.T.);
#2355=EDGE_CURVE('',#2762,#2768,#2976,.T.);
#2356=EDGE_CURVE('',#2768,#2769,#45,.T.);
#2357=EDGE_CURVE('',#2769,#2766,#2977,.T.);
#2358=EDGE_CURVE('',#2763,#2770,#2978,.T.);
#2359=EDGE_CURVE('',#2770,#2767,#675,.T.);
#2360=EDGE_CURVE('',#2757,#2771,#676,.T.);
#2361=EDGE_CURVE('',#2771,#2772,#2979,.T.);
#2362=EDGE_CURVE('',#2772,#2773,#2980,.T.);
#2363=EDGE_CURVE('',#2774,#2773,#46,.T.);
#2364=EDGE_CURVE('',#2764,#2774,#2981,.T.);
#2365=EDGE_CURVE('',#2770,#2758,#677,.T.);
#2366=EDGE_CURVE('',#2768,#2774,#2982,.T.);
#2367=EDGE_CURVE('',#2775,#2776,#678,.T.);
#2368=EDGE_CURVE('',#2776,#2775,#679,.T.);
#2369=EDGE_CURVE('',#2777,#2777,#556,.T.);
#2370=EDGE_CURVE('',#2778,#2778,#557,.T.);
#2371=EDGE_CURVE('',#2769,#2773,#2983,.T.);
#2372=EDGE_CURVE('',#2772,#2779,#558,.T.);
#2373=EDGE_CURVE('',#2780,#2779,#559,.T.);
#2374=EDGE_CURVE('',#2780,#2766,#560,.T.);
#2375=EDGE_CURVE('',#2765,#2781,#680,.T.);
#2376=EDGE_CURVE('',#2781,#2780,#2984,.T.);
#2377=EDGE_CURVE('',#2781,#2782,#681,.T.);
#2378=EDGE_CURVE('',#2782,#2771,#682,.T.);
#2379=EDGE_CURVE('',#2782,#2779,#2985,.T.);
#2380=EDGE_CURVE('',#2776,#2775,#47,.T.);
#2381=EDGE_CURVE('',#2783,#2784,#48,.T.);
#2382=EDGE_CURVE('',#2783,#2784,#683,.T.);
#2383=EDGE_CURVE('',#2785,#2786,#49,.T.);
#2384=EDGE_CURVE('',#2786,#2785,#684,.T.);
#2385=EDGE_CURVE('',#2787,#2787,#561,.T.);
#2386=EDGE_CURVE('',#2788,#2788,#562,.F.);
#2387=EDGE_CURVE('',#2789,#2789,#563,.T.);
#2388=EDGE_CURVE('',#2790,#2783,#564,.T.);
#2389=EDGE_CURVE('',#2784,#2791,#565,.T.);
#2390=EDGE_CURVE('',#2791,#2790,#685,.T.);
#2391=EDGE_CURVE('',#2792,#2793,#566,.T.);
#2392=EDGE_CURVE('',#2793,#2794,#686,.T.);
#2393=EDGE_CURVE('',#2794,#2795,#567,.T.);
#2394=EDGE_CURVE('',#2795,#2792,#687,.T.);
#2395=EDGE_CURVE('',#2794,#2793,#50,.F.);
#2396=EDGE_CURVE('',#2792,#2795,#51,.T.);
#2397=EDGE_CURVE('',#2791,#2790,#52,.F.);
#2398=EDGE_CURVE('',#2796,#2796,#568,.F.);
#2399=EDGE_CURVE('',#2797,#2797,#569,.T.);
#2400=EDGE_CURVE('',#2798,#2786,#688,.T.);
#2401=EDGE_CURVE('',#2785,#2799,#570,.T.);
#2402=EDGE_CURVE('',#2799,#2798,#689,.T.);
#2403=EDGE_CURVE('',#2800,#2800,#690,.T.);
#2404=EDGE_CURVE('',#2798,#2799,#53,.T.);
#2405=EDGE_CURVE('',#2801,#2802,#2986,.T.);
#2406=EDGE_CURVE('',#2803,#2802,#571,.T.);
#2407=EDGE_CURVE('',#2803,#2804,#2987,.T.);
#2408=EDGE_CURVE('',#2752,#2804,#2988,.T.);
#2409=EDGE_CURVE('',#2801,#2752,#2989,.T.);
#2410=EDGE_CURVE('',#2805,#2805,#572,.T.);
#2411=EDGE_CURVE('',#2806,#2806,#54,.F.);
#2412=EDGE_CURVE('',#2807,#2808,#55,.T.);
#2413=EDGE_CURVE('',#2809,#2807,#2990,.T.);
#2414=EDGE_CURVE('',#2810,#2809,#2991,.T.);
#2415=EDGE_CURVE('',#2811,#2810,#691,.T.);
#2416=EDGE_CURVE('',#2812,#2811,#2992,.T.);
#2417=EDGE_CURVE('',#2813,#2812,#692,.T.);
#2418=EDGE_CURVE('',#2802,#2813,#2993,.T.);
#2419=EDGE_CURVE('',#2808,#2801,#2994,.T.);
#2420=EDGE_CURVE('',#2803,#2814,#2995,.T.);
#2421=EDGE_CURVE('',#2813,#2814,#693,.T.);
#2422=EDGE_CURVE('',#2815,#2814,#694,.T.);
#2423=EDGE_CURVE('',#2816,#2815,#2996,.T.);
#2424=EDGE_CURVE('',#2817,#2816,#695,.T.);
#2425=EDGE_CURVE('',#2817,#2818,#2997,.T.);
#2426=EDGE_CURVE('',#2819,#2818,#2998,.T.);
#2427=EDGE_CURVE('',#2819,#2820,#56,.T.);
#2428=EDGE_CURVE('',#2820,#2804,#2999,.T.);
#2429=EDGE_CURVE('',#2820,#2808,#3000,.T.);
#2430=EDGE_CURVE('',#2821,#2821,#573,.T.);
#2431=EDGE_CURVE('',#2819,#2807,#3001,.T.);
#2432=EDGE_CURVE('',#2818,#2822,#574,.T.);
#2433=EDGE_CURVE('',#2823,#2822,#575,.T.);
#2434=EDGE_CURVE('',#2823,#2809,#576,.T.);
#2435=EDGE_CURVE('',#2824,#2823,#3002,.T.);
#2436=EDGE_CURVE('',#2810,#2824,#696,.T.);
#2437=EDGE_CURVE('',#2811,#2816,#577,.T.);
#2438=EDGE_CURVE('',#2825,#2824,#697,.T.);
#2439=EDGE_CURVE('',#2825,#2817,#698,.T.);
#2440=EDGE_CURVE('',#2815,#2812,#578,.T.);
#2441=EDGE_CURVE('',#2825,#2822,#3003,.T.);
#2752=VERTEX_POINT('',#8071);
#2753=VERTEX_POINT('',#8073);
#2754=VERTEX_POINT('',#8076);
#2755=VERTEX_POINT('',#8078);
#2756=VERTEX_POINT('',#8079);
#2757=VERTEX_POINT('',#8081);
#2758=VERTEX_POINT('',#8083);
#2759=VERTEX_POINT('',#8087);
#2760=VERTEX_POINT('',#8089);
#2761=VERTEX_POINT('',#8092);
#2762=VERTEX_POINT('',#8093);
#2763=VERTEX_POINT('',#8095);
#2764=VERTEX_POINT('',#8097);
#2765=VERTEX_POINT('',#8102);
#2766=VERTEX_POINT('',#8103);
#2767=VERTEX_POINT('',#8116);
#2768=VERTEX_POINT('',#8119);
#2769=VERTEX_POINT('',#8121);
#2770=VERTEX_POINT('',#8125);
#2771=VERTEX_POINT('',#8155);
#2772=VERTEX_POINT('',#8157);
#2773=VERTEX_POINT('',#8159);
#2774=VERTEX_POINT('',#8161);
#2775=VERTEX_POINT('',#8180);
#2776=VERTEX_POINT('',#8181);
#2777=VERTEX_POINT('',#8192);
#2778=VERTEX_POINT('',#8194);
#2779=VERTEX_POINT('',#8199);
#2780=VERTEX_POINT('',#8201);
#2781=VERTEX_POINT('',#8208);
#2782=VERTEX_POINT('',#8233);
#2783=VERTEX_POINT('',#8244);
#2784=VERTEX_POINT('',#8245);
#2785=VERTEX_POINT('',#8257);
#2786=VERTEX_POINT('',#8258);
#2787=VERTEX_POINT('',#8271);
#2788=VERTEX_POINT('',#8274);
#2789=VERTEX_POINT('',#8276);
#2790=VERTEX_POINT('',#8278);
#2791=VERTEX_POINT('',#8280);
#2792=VERTEX_POINT('',#8291);
#2793=VERTEX_POINT('',#8292);
#2794=VERTEX_POINT('',#8302);
#2795=VERTEX_POINT('',#8304);
#2796=VERTEX_POINT('',#8320);
#2797=VERTEX_POINT('',#8322);
#2798=VERTEX_POINT('',#8327);
#2799=VERTEX_POINT('',#8329);
#2800=VERTEX_POINT('',#8350);
#2801=VERTEX_POINT('',#8356);
#2802=VERTEX_POINT('',#8357);
#2803=VERTEX_POINT('',#8359);
#2804=VERTEX_POINT('',#8361);
#2805=VERTEX_POINT('',#8366);
#2806=VERTEX_POINT('',#8371);
#2807=VERTEX_POINT('',#8375);
#2808=VERTEX_POINT('',#8376);
#2809=VERTEX_POINT('',#8378);
#2810=VERTEX_POINT('',#8380);
#2811=VERTEX_POINT('',#8387);
#2812=VERTEX_POINT('',#8389);
#2813=VERTEX_POINT('',#8395);
#2814=VERTEX_POINT('',#8400);
#2815=VERTEX_POINT('',#8430);
#2816=VERTEX_POINT('',#8432);
#2817=VERTEX_POINT('',#8438);
#2818=VERTEX_POINT('',#8440);
#2819=VERTEX_POINT('',#8442);
#2820=VERTEX_POINT('',#8444);
#2821=VERTEX_POINT('',#8450);
#2822=VERTEX_POINT('',#8455);
#2823=VERTEX_POINT('',#8457);
#2824=VERTEX_POINT('',#8461);
#2825=VERTEX_POINT('',#8490);
#2968=LINE('',#8077,#3146);
#2969=LINE('',#8082,#3147);
#2970=LINE('',#8091,#3148);
#2971=LINE('',#8096,#3149);
#2972=LINE('',#8098,#3150);
#2973=LINE('',#8099,#3151);
#2974=LINE('',#8101,#3152);
#2975=LINE('',#8117,#3153);
#2976=LINE('',#8118,#3154);
#2977=LINE('',#8122,#3155);
#2978=LINE('',#8124,#3156);
#2979=LINE('',#8156,#3157);
#2980=LINE('',#8158,#3158);
#2981=LINE('',#8162,#3159);
#2982=LINE('',#8169,#3160);
#2983=LINE('',#8196,#3161);
#2984=LINE('',#8209,#3162);
#2985=LINE('',#8240,#3163);
#2986=LINE('',#8355,#3164);
#2987=LINE('',#8360,#3165);
#2988=LINE('',#8362,#3166);
#2989=LINE('',#8363,#3167);
#2990=LINE('',#8377,#3168);
#2991=LINE('',#8379,#3169);
#2992=LINE('',#8388,#3170);
#2993=LINE('',#8396,#3171);
#2994=LINE('',#8397,#3172);
#2995=LINE('',#8399,#3173);
#2996=LINE('',#8431,#3174);
#2997=LINE('',#8439,#3175);
#2998=LINE('',#8441,#3176);
#2999=LINE('',#8445,#3177);
#3000=LINE('',#8447,#3178);
#3001=LINE('',#8452,#3179);
#3002=LINE('',#8460,#3180);
#3003=LINE('',#8499,#3181);
#3146=VECTOR('',#6162,1.);
#3147=VECTOR('',#6165,1.);
#3148=VECTOR('',#6176,1.);
#3149=VECTOR('',#6179,1.);
#3150=VECTOR('',#6180,1.);
#3151=VECTOR('',#6181,1.);
#3152=VECTOR('',#6184,1.);
#3153=VECTOR('',#6185,1.);
#3154=VECTOR('',#6186,1.);
#3155=VECTOR('',#6189,1.);
#3156=VECTOR('',#6192,1.);
#3157=VECTOR('',#6195,1.);
#3158=VECTOR('',#6196,1.);
#3159=VECTOR('',#6199,1.);
#3160=VECTOR('',#6202,1.);
#3161=VECTOR('',#6211,1.);
#3162=VECTOR('',#6222,1.);
#3163=VECTOR('',#6229,1.);
#3164=VECTOR('',#6284,1.);
#3165=VECTOR('',#6287,1.);
#3166=VECTOR('',#6288,1.);
#3167=VECTOR('',#6289,1.);
#3168=VECTOR('',#6308,1.);
#3169=VECTOR('',#6309,1.);
#3170=VECTOR('',#6310,1.);
#3171=VECTOR('',#6311,1.);
#3172=VECTOR('',#6312,1.);
#3173=VECTOR('',#6315,1.);
#3174=VECTOR('',#6318,1.);
#3175=VECTOR('',#6319,1.);
#3176=VECTOR('',#6320,1.);
#3177=VECTOR('',#6323,1.);
#3178=VECTOR('',#6326,1.);
#3179=VECTOR('',#6333,1.);
#3180=VECTOR('',#6344,1.);
#3181=VECTOR('',#6357,1.);
#3490=EDGE_LOOP('',(#1635));
#3491=EDGE_LOOP('',(#1636));
#3492=EDGE_LOOP('',(#1637));
#3493=EDGE_LOOP('',(#1638,#1639,#1640,#1641));
#3494=EDGE_LOOP('',(#1642));
#3495=EDGE_LOOP('',(#1643));
#3496=EDGE_LOOP('',(#1644,#1645,#1646,#1647,#1648,#1649));
#3497=EDGE_LOOP('',(#1650,#1651,#1652,#1653,#1654,#1655,#1656,#1657,#1658));
#3498=EDGE_LOOP('',(#1659,#1660,#1661,#1662));
#3499=EDGE_LOOP('',(#1663,#1664,#1665,#1666,#1667,#1668,#1669,#1670,#1671));
#3500=EDGE_LOOP('',(#1672,#1673,#1674,#1675,#1676));
#3501=EDGE_LOOP('',(#1677,#1678));
#3502=EDGE_LOOP('',(#1679));
#3503=EDGE_LOOP('',(#1680));
#3504=EDGE_LOOP('',(#1681,#1682,#1683,#1684));
#3505=EDGE_LOOP('',(#1685,#1686,#1687,#1688,#1689,#1690));
#3506=EDGE_LOOP('',(#1691,#1692,#1693,#1694));
#3507=EDGE_LOOP('',(#1695,#1696,#1697,#1698,#1699,#1700));
#3508=EDGE_LOOP('',(#1701,#1702,#1703,#1704));
#3509=EDGE_LOOP('',(#1705,#1706,#1707,#1708));
#3510=EDGE_LOOP('',(#1709,#1710));
#3511=EDGE_LOOP('',(#1711,#1712));
#3512=EDGE_LOOP('',(#1713,#1714));
#3513=EDGE_LOOP('',(#1715,#1716));
#3514=EDGE_LOOP('',(#1717,#1718,#1719,#1720));
#3515=EDGE_LOOP('',(#1721));
#3516=EDGE_LOOP('',(#1722));
#3517=EDGE_LOOP('',(#1723));
#3518=EDGE_LOOP('',(#1724));
#3519=EDGE_LOOP('',(#1725,#1726,#1727,#1728));
#3520=EDGE_LOOP('',(#1729,#1730,#1731,#1732));
#3521=EDGE_LOOP('',(#1733,#1734,#1735,#1736));
#3522=EDGE_LOOP('',(#1737,#1738,#1739,#1740));
#3523=EDGE_LOOP('',(#1741));
#3524=EDGE_LOOP('',(#1742));
#3525=EDGE_LOOP('',(#1743,#1744,#1745,#1746));
#3526=EDGE_LOOP('',(#1747));
#3527=EDGE_LOOP('',(#1748));
#3528=EDGE_LOOP('',(#1749,#1750,#1751,#1752));
#3529=EDGE_LOOP('',(#1753));
#3530=EDGE_LOOP('',(#1754));
#3531=EDGE_LOOP('',(#1755,#1756,#1757,#1758,#1759,#1760));
#3532=EDGE_LOOP('',(#1761));
#3533=EDGE_LOOP('',(#1762));
#3534=EDGE_LOOP('',(#1763,#1764));
#3535=EDGE_LOOP('',(#1765,#1766));
#3536=EDGE_LOOP('',(#1767));
#3537=EDGE_LOOP('',(#1768,#1769));
#3538=EDGE_LOOP('',(#1770,#1771));
#3539=EDGE_LOOP('',(#1772,#1773,#1774,#1775,#1776,#1777,#1778,#1779,#1780));
#3540=EDGE_LOOP('',(#1781,#1782,#1783,#1784));
#3541=EDGE_LOOP('',(#1785,#1786,#1787,#1788,#1789,#1790,#1791,#1792,#1793));
#3542=EDGE_LOOP('',(#1794,#1795,#1796,#1797,#1798));
#3543=EDGE_LOOP('',(#1799));
#3544=EDGE_LOOP('',(#1800));
#3545=EDGE_LOOP('',(#1801,#1802,#1803,#1804));
#3546=EDGE_LOOP('',(#1805,#1806,#1807,#1808,#1809,#1810));
#3547=EDGE_LOOP('',(#1811,#1812,#1813,#1814));
#3548=EDGE_LOOP('',(#1815,#1816,#1817,#1818,#1819,#1820));
#3549=EDGE_LOOP('',(#1821));
#3550=EDGE_LOOP('',(#1822,#1823,#1824,#1825));
#3551=EDGE_LOOP('',(#1826,#1827,#1828,#1829));
#3552=EDGE_LOOP('',(#1830,#1831,#1832,#1833));
#3553=EDGE_LOOP('',(#1834,#1835,#1836,#1837));
#3554=EDGE_LOOP('',(#1838));
#3555=EDGE_LOOP('',(#1839));
#3556=EDGE_LOOP('',(#1840));
#3557=EDGE_LOOP('',(#1841));
#3558=EDGE_LOOP('',(#1842));
#3559=EDGE_LOOP('',(#1843));
#3560=EDGE_LOOP('',(#1844));
#3867=FACE_BOUND('',#3490,.T.);
#3868=FACE_BOUND('',#3491,.T.);
#3869=FACE_BOUND('',#3492,.T.);
#3870=FACE_BOUND('',#3493,.T.);
#3871=FACE_BOUND('',#3494,.T.);
#3872=FACE_BOUND('',#3495,.T.);
#3873=FACE_BOUND('',#3496,.T.);
#3874=FACE_BOUND('',#3497,.T.);
#3875=FACE_BOUND('',#3498,.T.);
#3876=FACE_BOUND('',#3499,.T.);
#3877=FACE_BOUND('',#3500,.T.);
#3878=FACE_BOUND('',#3501,.T.);
#3879=FACE_BOUND('',#3502,.T.);
#3880=FACE_BOUND('',#3503,.T.);
#3881=FACE_BOUND('',#3504,.T.);
#3882=FACE_BOUND('',#3505,.T.);
#3883=FACE_BOUND('',#3506,.T.);
#3884=FACE_BOUND('',#3507,.T.);
#3885=FACE_BOUND('',#3508,.T.);
#3886=FACE_BOUND('',#3509,.T.);
#3887=FACE_BOUND('',#3510,.T.);
#3888=FACE_BOUND('',#3511,.T.);
#3889=FACE_BOUND('',#3512,.T.);
#3890=FACE_BOUND('',#3513,.T.);
#3891=FACE_BOUND('',#3514,.T.);
#3892=FACE_BOUND('',#3515,.T.);
#3893=FACE_BOUND('',#3516,.T.);
#3894=FACE_BOUND('',#3517,.T.);
#3895=FACE_BOUND('',#3518,.T.);
#3896=FACE_BOUND('',#3519,.T.);
#3897=FACE_BOUND('',#3520,.T.);
#3898=FACE_BOUND('',#3521,.T.);
#3899=FACE_BOUND('',#3522,.T.);
#3900=FACE_BOUND('',#3523,.T.);
#3901=FACE_BOUND('',#3524,.T.);
#3902=FACE_BOUND('',#3525,.T.);
#3903=FACE_BOUND('',#3526,.T.);
#3904=FACE_BOUND('',#3527,.T.);
#3905=FACE_BOUND('',#3528,.T.);
#3906=FACE_BOUND('',#3529,.T.);
#3907=FACE_BOUND('',#3530,.T.);
#3908=FACE_BOUND('',#3531,.T.);
#3909=FACE_BOUND('',#3532,.T.);
#3910=FACE_BOUND('',#3533,.T.);
#3911=FACE_BOUND('',#3534,.T.);
#3912=FACE_BOUND('',#3535,.T.);
#3913=FACE_BOUND('',#3536,.T.);
#3914=FACE_BOUND('',#3537,.T.);
#3915=FACE_BOUND('',#3538,.T.);
#3916=FACE_BOUND('',#3539,.T.);
#3917=FACE_BOUND('',#3540,.T.);
#3918=FACE_BOUND('',#3541,.T.);
#3919=FACE_BOUND('',#3542,.T.);
#3920=FACE_BOUND('',#3543,.T.);
#3921=FACE_BOUND('',#3544,.T.);
#3922=FACE_BOUND('',#3545,.T.);
#3923=FACE_BOUND('',#3546,.T.);
#3924=FACE_BOUND('',#3547,.T.);
#3925=FACE_BOUND('',#3548,.T.);
#3926=FACE_BOUND('',#3549,.T.);
#3927=FACE_BOUND('',#3550,.T.);
#3928=FACE_BOUND('',#3551,.T.);
#3929=FACE_BOUND('',#3552,.T.);
#3930=FACE_BOUND('',#3553,.T.);
#3931=FACE_BOUND('',#3554,.T.);
#3932=FACE_BOUND('',#3555,.T.);
#3933=FACE_BOUND('',#3556,.T.);
#3934=FACE_BOUND('',#3557,.T.);
#3935=FACE_BOUND('',#3558,.T.);
#3936=FACE_BOUND('',#3559,.T.);
#3937=FACE_BOUND('',#3560,.T.);
#4014=PLANE('',#4964);
#4015=PLANE('',#4971);
#4016=PLANE('',#4973);
#4017=PLANE('',#4976);
#4018=PLANE('',#4978);
#4019=PLANE('',#4983);
#4020=PLANE('',#5016);
#4021=PLANE('',#5017);
#4022=PLANE('',#5019);
#4023=PLANE('',#5026);
#4024=PLANE('',#5029);
#4025=PLANE('',#5031);
#4026=PLANE('',#5035);
#4027=PLANE('',#5042);
#4028=PLANE('',#5047);
#4029=PLANE('',#5048);
#4030=PLANE('',#5049);
#4031=PLANE('',#5050);
#4270=ADVANCED_FACE('',(#3867,#3868),#281,.T.);
#4271=ADVANCED_FACE('',(#3869,#3870),#4014,.T.);
#4272=ADVANCED_FACE('',(#3871,#3872),#282,.T.);
#4273=ADVANCED_FACE('',(#3873),#4015,.F.);
#4274=ADVANCED_FACE('',(#3874),#4016,.T.);
#4275=ADVANCED_FACE('',(#3875),#283,.T.);
#4276=ADVANCED_FACE('',(#3876),#4017,.T.);
#4277=ADVANCED_FACE('',(#3877),#4018,.F.);
#4278=ADVANCED_FACE('',(#3878,#3879,#3880),#284,.T.);
#4279=ADVANCED_FACE('',(#3881),#285,.F.);
#4280=ADVANCED_FACE('',(#3882),#4019,.F.);
#4281=ADVANCED_FACE('',(#3883),#286,.T.);
#4282=ADVANCED_FACE('',(#3884),#200,.T.);
#4283=ADVANCED_FACE('',(#3885),#201,.T.);
#4284=ADVANCED_FACE('',(#3886),#287,.T.);
#4285=ADVANCED_FACE('',(#3887,#3888),#288,.F.);
#4286=ADVANCED_FACE('',(#3889,#3890),#289,.F.);
#4287=ADVANCED_FACE('',(#3891),#290,.T.);
#4288=ADVANCED_FACE('',(#3892,#3893),#291,.T.);
#4289=ADVANCED_FACE('',(#3894,#3895,#3896,#3897),#292,.T.);
#4290=ADVANCED_FACE('',(#3898,#3899),#293,.F.);
#4291=ADVANCED_FACE('',(#3900,#3901,#3902,#3903),#294,.T.);
#4292=ADVANCED_FACE('',(#3904,#3905),#295,.F.);
#4293=ADVANCED_FACE('',(#3906,#3907),#4020,.F.);
#4294=ADVANCED_FACE('',(#3908),#4021,.F.);
#4295=ADVANCED_FACE('',(#3909,#3910),#4022,.T.);
#4296=ADVANCED_FACE('',(#3911),#296,.F.);
#4297=ADVANCED_FACE('',(#3912),#297,.F.);
#4298=ADVANCED_FACE('',(#3913,#3914),#298,.F.);
#4299=ADVANCED_FACE('',(#3915),#299,.F.);
#4300=ADVANCED_FACE('',(#3916),#4023,.T.);
#4301=ADVANCED_FACE('',(#3917),#300,.T.);
#4302=ADVANCED_FACE('',(#3918),#4024,.T.);
#4303=ADVANCED_FACE('',(#3919),#4025,.F.);
#4304=ADVANCED_FACE('',(#3920,#3921),#301,.T.);
#4305=ADVANCED_FACE('',(#3922),#302,.F.);
#4306=ADVANCED_FACE('',(#3923),#4026,.F.);
#4307=ADVANCED_FACE('',(#3924),#303,.T.);
#4308=ADVANCED_FACE('',(#3925),#202,.T.);
#4309=ADVANCED_FACE('',(#3926,#3927),#4027,.T.);
#4310=ADVANCED_FACE('',(#3928),#203,.T.);
#4311=ADVANCED_FACE('',(#3929),#304,.T.);
#4312=ADVANCED_FACE('',(#3930),#305,.T.);
#4313=ADVANCED_FACE('',(#3931,#3932),#4028,.F.);
#4314=ADVANCED_FACE('',(#3933),#4029,.F.);
#4315=ADVANCED_FACE('',(#3934,#3935),#4030,.T.);
#4316=ADVANCED_FACE('',(#3936,#3937),#4031,.F.);
#4332=CLOSED_SHELL('',(#4270,#4271,#4272,#4273,#4274,#4275,#4276,#4277,
#4278,#4279,#4280,#4281,#4282,#4283,#4284,#4285,#4286,#4287,#4288,#4289,
#4290,#4291,#4292,#4293,#4294,#4295,#4296,#4297,#4298,#4299,#4300,#4301,
#4302,#4303,#4304,#4305,#4306,#4307,#4308,#4309,#4310,#4311,#4312,#4313,
#4314,#4315,#4316));
#4343=STYLED_ITEM('',(#4354),#4458);
#4354=PRESENTATION_STYLE_ASSIGNMENT((#4370));
#4370=SURFACE_STYLE_USAGE(.BOTH.,#4386);
#4386=SURFACE_SIDE_STYLE('',(#4402));
#4402=SURFACE_STYLE_FILL_AREA(#4418);
#4418=FILL_AREA_STYLE('',(#4434));
#4434=FILL_AREA_STYLE_COLOUR('',#4447);
#4447=COLOUR_RGB('', 0.72549020, 0.75294118, 0.79215686);
#4458=MANIFOLD_SOLID_BREP('CRANKSHAFT',#4332);
#4470=SHAPE_DEFINITION_REPRESENTATION(#8584,#4482);
#4482=SHAPE_REPRESENTATION('CRANKSHAFT',(#4484),#8545);
#4484=AXIS2_PLACEMENT_3D('',#6402,#5064,#5065);
#4961=AXIS2_PLACEMENT_3D('',#8069,#6152,#6153);
#4962=AXIS2_PLACEMENT_3D('',#8070,#6154,#6155);
#4963=AXIS2_PLACEMENT_3D('',#8072,#6156,#6157);
#4964=AXIS2_PLACEMENT_3D('',#8074,#6158,#6159);
#4965=AXIS2_PLACEMENT_3D('',#8075,#6160,#6161);
#4966=AXIS2_PLACEMENT_3D('',#8080,#6163,#6164);
#4967=AXIS2_PLACEMENT_3D('',#8084,#6166,#6167);
#4968=AXIS2_PLACEMENT_3D('',#8085,#6168,#6169);
#4969=AXIS2_PLACEMENT_3D('',#8086,#6170,#6171);
#4970=AXIS2_PLACEMENT_3D('',#8088,#6172,#6173);
#4971=AXIS2_PLACEMENT_3D('',#8090,#6174,#6175);
#4972=AXIS2_PLACEMENT_3D('',#8094,#6177,#6178);
#4973=AXIS2_PLACEMENT_3D('',#8100,#6182,#6183);
#4974=AXIS2_PLACEMENT_3D('',#8120,#6187,#6188);
#4975=AXIS2_PLACEMENT_3D('',#8123,#6190,#6191);
#4976=AXIS2_PLACEMENT_3D('',#8148,#6193,#6194);
#4977=AXIS2_PLACEMENT_3D('',#8160,#6197,#6198);
#4978=AXIS2_PLACEMENT_3D('',#8168,#6200,#6201);
#4979=AXIS2_PLACEMENT_3D('',#8170,#6203,#6204);
#4980=AXIS2_PLACEMENT_3D('',#8191,#6205,#6206);
#4981=AXIS2_PLACEMENT_3D('',#8193,#6207,#6208);
#4982=AXIS2_PLACEMENT_3D('',#8195,#6209,#6210);
#4983=AXIS2_PLACEMENT_3D('',#8197,#6212,#6213);
#4984=AXIS2_PLACEMENT_3D('',#8198,#6214,#6215);
#4985=AXIS2_PLACEMENT_3D('',#8200,#6216,#6217);
#4986=AXIS2_PLACEMENT_3D('',#8202,#6218,#6219);
#4987=AXIS2_PLACEMENT_3D('',#8203,#6220,#6221);
#4988=AXIS2_PLACEMENT_3D('',#8210,#6223,#6224);
#4989=AXIS2_PLACEMENT_3D('',#8238,#6225,#6226);
#4990=AXIS2_PLACEMENT_3D('',#8239,#6227,#6228);
#4991=AXIS2_PLACEMENT_3D('',#8241,#6230,#6231);
#4992=AXIS2_PLACEMENT_3D('',#8242,#6232,#6233);
#4993=AXIS2_PLACEMENT_3D('',#8243,#6234,#6235);
#4994=AXIS2_PLACEMENT_3D('',#8255,#6236,#6237);
#4995=AXIS2_PLACEMENT_3D('',#8256,#6238,#6239);
#4996=AXIS2_PLACEMENT_3D('',#8268,#6240,#6241);
#4997=AXIS2_PLACEMENT_3D('',#8269,#6242,#6243);
#4998=AXIS2_PLACEMENT_3D('',#8270,#6244,#6245);
#4999=AXIS2_PLACEMENT_3D('',#8272,#6246,#6247);
#5000=AXIS2_PLACEMENT_3D('',#8273,#6248,#6249);
#5001=AXIS2_PLACEMENT_3D('',#8275,#6250,#6251);
#5002=AXIS2_PLACEMENT_3D('',#8277,#6252,#6253);
#5003=AXIS2_PLACEMENT_3D('',#8279,#6254,#6255);
#5004=AXIS2_PLACEMENT_3D('',#8290,#6256,#6257);
#5005=AXIS2_PLACEMENT_3D('',#8303,#6258,#6259);
#5006=AXIS2_PLACEMENT_3D('',#8314,#6260,#6261);
#5007=AXIS2_PLACEMENT_3D('',#8315,#6262,#6263);
#5008=AXIS2_PLACEMENT_3D('',#8316,#6264,#6265);
#5009=AXIS2_PLACEMENT_3D('',#8317,#6266,#6267);
#5010=AXIS2_PLACEMENT_3D('',#8318,#6268,#6269);
#5011=AXIS2_PLACEMENT_3D('',#8319,#6270,#6271);
#5012=AXIS2_PLACEMENT_3D('',#8321,#6272,#6273);
#5013=AXIS2_PLACEMENT_3D('',#8328,#6274,#6275);
#5014=AXIS2_PLACEMENT_3D('',#8351,#6276,#6277);
#5015=AXIS2_PLACEMENT_3D('',#8352,#6278,#6279);
#5016=AXIS2_PLACEMENT_3D('',#8353,#6280,#6281);
#5017=AXIS2_PLACEMENT_3D('',#8354,#6282,#6283);
#5018=AXIS2_PLACEMENT_3D('',#8358,#6285,#6286);
#5019=AXIS2_PLACEMENT_3D('',#8364,#6290,#6291);
#5020=AXIS2_PLACEMENT_3D('',#8365,#6292,#6293);
#5021=AXIS2_PLACEMENT_3D('',#8367,#6294,#6295);
#5022=AXIS2_PLACEMENT_3D('',#8368,#6296,#6297);
#5023=AXIS2_PLACEMENT_3D('',#8369,#6298,#6299);
#5024=AXIS2_PLACEMENT_3D('',#8370,#6300,#6301);
#5025=AXIS2_PLACEMENT_3D('',#8372,#6302,#6303);
#5026=AXIS2_PLACEMENT_3D('',#8373,#6304,#6305);
#5027=AXIS2_PLACEMENT_3D('',#8374,#6306,#6307);
#5028=AXIS2_PLACEMENT_3D('',#8398,#6313,#6314);
#5029=AXIS2_PLACEMENT_3D('',#8423,#6316,#6317);
#5030=AXIS2_PLACEMENT_3D('',#8443,#6321,#6322);
#5031=AXIS2_PLACEMENT_3D('',#8446,#6324,#6325);
#5032=AXIS2_PLACEMENT_3D('',#8448,#6327,#6328);
#5033=AXIS2_PLACEMENT_3D('',#8449,#6329,#6330);
#5034=AXIS2_PLACEMENT_3D('',#8451,#6331,#6332);
#5035=AXIS2_PLACEMENT_3D('',#8453,#6334,#6335);
#5036=AXIS2_PLACEMENT_3D('',#8454,#6336,#6337);
#5037=AXIS2_PLACEMENT_3D('',#8456,#6338,#6339);
#5038=AXIS2_PLACEMENT_3D('',#8458,#6340,#6341);
#5039=AXIS2_PLACEMENT_3D('',#8459,#6342,#6343);
#5040=AXIS2_PLACEMENT_3D('',#8466,#6345,#6346);
#5041=AXIS2_PLACEMENT_3D('',#8467,#6347,#6348);
#5042=AXIS2_PLACEMENT_3D('',#8495,#6349,#6350);
#5043=AXIS2_PLACEMENT_3D('',#8496,#6351,#6352);
#5044=AXIS2_PLACEMENT_3D('',#8497,#6353,#6354);
#5045=AXIS2_PLACEMENT_3D('',#8498,#6355,#6356);
#5046=AXIS2_PLACEMENT_3D('',#8500,#6358,#6359);
#5047=AXIS2_PLACEMENT_3D('',#8501,#6360,#6361);
#5048=AXIS2_PLACEMENT_3D('',#8502,#6362,#6363);
#5049=AXIS2_PLACEMENT_3D('',#8503,#6364,#6365);
#5050=AXIS2_PLACEMENT_3D('',#8504,#6366,#6367);
#5064=DIRECTION('',(0.,0.,1.));
#5065=DIRECTION('',(1.,0.,0.));
#6152=DIRECTION('',(0.,0.,-1.));
#6153=DIRECTION('',(1.,0.,0.));
#6154=DIRECTION('',(0.,0.,1.));
#6155=DIRECTION('',(-3.22276666936548E-17,-1.,0.));
#6156=DIRECTION('',(0.,0.,1.));
#6157=DIRECTION('',(1.,0.,0.));
#6158=DIRECTION('',(0.,0.,1.));
#6159=DIRECTION('',(1.,0.,0.));
#6160=DIRECTION('',(0.,0.,-1.));
#6161=DIRECTION('',(0.,-1.,0.));
#6162=DIRECTION('',(-0.165120262618152,-0.986273440214686,0.));
#6163=DIRECTION('',(0.,0.,-1.));
#6164=DIRECTION('',(0.997579197588362,0.0695395178223138,0.));
#6165=DIRECTION('',(-0.165120262618151,0.986273440214686,0.));
#6166=DIRECTION('',(0.,0.,-1.));
#6167=DIRECTION('',(-0.965831339887295,0.259171416038716,0.));
#6168=DIRECTION('',(0.,0.,-1.));
#6169=DIRECTION('',(1.,0.,0.));
#6170=DIRECTION('',(0.,0.,1.));
#6171=DIRECTION('',(1.,0.,0.));
#6172=DIRECTION('',(0.,0.,1.));
#6173=DIRECTION('',(1.,0.,0.));
#6174=DIRECTION('',(0.,0.,1.));
#6175=DIRECTION('',(1.,0.,0.));
#6176=DIRECTION('',(-0.165120262618152,-0.986273440214686,0.));
#6177=DIRECTION('',(0.,0.,1.));
#6178=DIRECTION('',(0.986273440214687,0.165120262618151,0.));
#6179=DIRECTION('',(-0.165120262618151,0.986273440214686,0.));
#6180=DIRECTION('',(1.,0.,0.));
#6181=DIRECTION('',(1.,0.,0.));
#6182=DIRECTION('',(-0.986273440214686,0.165120262618152,0.));
#6183=DIRECTION('',(-0.165120262618152,-0.986273440214686,0.));
#6184=DIRECTION('',(-3.5527136788005E-16,-7.105427357601E-16,-1.));
#6185=DIRECTION('',(0.,0.,1.));
#6186=DIRECTION('',(-0.143488198627506,-0.85706379729923,0.494826014083393));
#6187=DIRECTION('',(0.986273440214686,-0.165120262618152,6.12323399573663E-17));
#6188=DIRECTION('',(-0.165120262618152,-0.986273440214686,-1.60794481439885E-13));
#6189=DIRECTION('',(-0.165120262618152,-0.986273440214686,0.));
#6190=DIRECTION('',(0.,0.,-1.));
#6191=DIRECTION('',(1.,0.,0.));
#6192=DIRECTION('',(0.,0.,1.));
#6193=DIRECTION('',(0.986273440214686,0.165120262618151,0.));
#6194=DIRECTION('',(-0.165120262618151,0.986273440214686,0.));
#6195=DIRECTION('',(-3.5527136788005E-16,7.105427357601E-16,-1.));
#6196=DIRECTION('',(-0.165120262618151,0.986273440214686,0.));
#6197=DIRECTION('',(0.986273440214686,0.165120262618152,6.12323399573648E-17));
#6198=DIRECTION('',(0.165120262618152,-0.986273440214686,1.37737697698504E-13));
#6199=DIRECTION('',(0.143488198627506,-0.85706379729923,0.494826014083392));
#6200=DIRECTION('',(0.,0.5,0.866025403784439));
#6201=DIRECTION('',(0.,-0.866025403784439,0.5));
#6202=DIRECTION('',(1.,0.,0.));
#6203=DIRECTION('',(0.,0.,-1.));
#6204=DIRECTION('',(-1.,0.,0.));
#6205=DIRECTION('',(0.,0.,1.));
#6206=DIRECTION('',(1.,0.,0.));
#6207=DIRECTION('',(0.,0.,1.));
#6208=DIRECTION('',(1.,0.,0.));
#6209=DIRECTION('',(-1.,0.,0.));
#6210=DIRECTION('',(0.,0.,-1.));
#6211=DIRECTION('',(1.,0.,0.));
#6212=DIRECTION('',(0.,0.,1.));
#6213=DIRECTION('',(1.,0.,0.));
#6214=DIRECTION('',(0.,0.,-1.));
#6215=DIRECTION('',(0.986273440214686,0.165120262618156,0.));
#6216=DIRECTION('',(0.,0.,1.));
#6217=DIRECTION('',(-0.939132344209142,-0.343555585109953,0.));
#6218=DIRECTION('',(0.,0.,-1.));
#6219=DIRECTION('',(-0.93913234420914,-0.343555585109957,0.));
#6220=DIRECTION('',(-4.7167604994452E-18,4.7167604994452E-18,1.));
#6221=DIRECTION('',(-0.939132344209142,-0.343555585109952,-2.80919293170665E-18));
#6222=DIRECTION('',(0.,0.,-1.));
#6223=DIRECTION('',(0.,0.,-1.));
#6224=DIRECTION('',(1.,-6.12323399573677E-17,0.));
#6225=DIRECTION('',(0.,0.,-1.));
#6226=DIRECTION('',(1.,-6.12323399573677E-17,0.));
#6227=DIRECTION('',(-2.46519032881566E-34,-9.43119924304831E-18,1.));
#6228=DIRECTION('',(0.986273440214686,0.165120262618152,1.55728209581625E-18));
#6229=DIRECTION('',(0.,0.,-1.));
#6230=DIRECTION('',(0.,-0.888557159765258,-0.458765924878798));
#6231=DIRECTION('',(0.,-0.458765924878798,0.888557159765258));
#6232=DIRECTION('',(-7.09909674989915E-15,0.009750455400229,-0.99995246317987));
#6233=DIRECTION('',(-1.52981362508847E-13,0.99995246317987,0.009750455400229));
#6234=DIRECTION('',(-1.97831778091143E-14,0.236053850037173,-0.971739975447459));
#6235=DIRECTION('',(-5.82449999783108E-15,0.971739975447459,0.236053850037173));
#6236=DIRECTION('',(0.,-0.897334135151735,0.441351843648));
#6237=DIRECTION('',(0.,0.441351843648,0.897334135151735));
#6238=DIRECTION('',(-3.30575397759658E-16,-0.226567721496539,-0.973995414555873));
#6239=DIRECTION('',(-9.67639922184483E-15,0.973995414555873,-0.226567721496539));
#6240=DIRECTION('',(0.,0.,-1.));
#6241=DIRECTION('',(1.,0.,0.));
#6242=DIRECTION('',(0.,0.,1.));
#6243=DIRECTION('',(0.,-1.,0.));
#6244=DIRECTION('',(0.,0.,1.));
#6245=DIRECTION('',(5.73018335290403E-17,1.,0.));
#6246=DIRECTION('',(0.,0.,1.));
#6247=DIRECTION('',(-1.,0.,0.));
#6248=DIRECTION('',(0.,-1.48882899694033E-16,1.));
#6249=DIRECTION('',(0.,-1.,-1.48882899694033E-16));
#6250=DIRECTION('',(0.,0.,1.));
#6251=DIRECTION('',(-1.,-1.8367567571222E-16,0.));
#6252=DIRECTION('',(0.101700025524789,0.994815108822059,-6.37778367330008E-5));
#6253=DIRECTION('',(-0.973565999163698,0.0995145471552375,-0.205587208203424));
#6254=DIRECTION('',(-0.101703879828654,0.994814714812882,-6.34000234451596E-5));
#6255=DIRECTION('',(0.994735072765686,0.101696543707177,0.0126470553038893));
#6256=DIRECTION('',(-0.101686733058552,-0.99481646753779,6.50808128760761E-5));
#6257=DIRECTION('',(0.994736828143844,-0.101679419936604,-0.0126466713280615));
#6258=DIRECTION('',(0.101687994499013,-0.994816338604938,6.49571619446657E-5));
#6259=DIRECTION('',(-0.973567282668449,-0.0995025376029421,0.205586942990423));
#6260=DIRECTION('',(0.,-1.,0.));
#6261=DIRECTION('',(0.,0.,1.));
#6262=DIRECTION('',(0.,-0.971739975447459,-0.236053850037172));
#6263=DIRECTION('',(0.,-0.236053850037173,0.971739975447459));
#6264=DIRECTION('',(3.44043640502547E-16,0.236053850037172,-0.971739975447459));
#6265=DIRECTION('',(3.64515562786427E-14,0.971739975447459,0.236053850037172));
#6266=DIRECTION('',(0.,-0.971739975447459,-0.236053850037172));
#6267=DIRECTION('',(0.,0.236053850037173,-0.971739975447459));
#6268=DIRECTION('',(0.,0.,-1.));
#6269=DIRECTION('',(1.,0.,0.));
#6270=DIRECTION('',(0.,0.,-1.));
#6271=DIRECTION('',(-1.,0.,0.));
#6272=DIRECTION('',(-2.45014736469E-16,-2.45014736469E-16,-1.));
#6273=DIRECTION('',(1.,-1.8367567571222E-16,-2.45014736469E-16));
#6274=DIRECTION('',(0.101527794842484,0.994832700123817,7.50917920324775E-5));
#6275=DIRECTION('',(-0.994759690413714,0.101521257725348,-0.0121075413637714));
#6276=DIRECTION('',(0.,-1.,0.));
#6277=DIRECTION('',(0.,0.,1.));
#6278=DIRECTION('',(0.,-0.973995414555873,0.226567721496538));
#6279=DIRECTION('',(0.,-0.226567721496537,-0.973995414555873));
#6280=DIRECTION('',(0.,0.,-1.));
#6281=DIRECTION('',(0.,-1.,0.));
#6282=DIRECTION('',(0.,0.,-1.));
#6283=DIRECTION('',(-1.,0.,0.));
#6284=DIRECTION('',(-0.165120262618151,0.986273440214686,0.));
#6285=DIRECTION('',(0.,0.,-1.));
#6286=DIRECTION('',(-0.986273440214686,0.165120262618152,0.));
#6287=DIRECTION('',(-0.165120262618152,-0.986273440214686,0.));
#6288=DIRECTION('',(-1.,0.,0.));
#6289=DIRECTION('',(-1.,0.,0.));
#6290=DIRECTION('',(0.,0.,-1.));
#6291=DIRECTION('',(0.,-1.,0.));
#6292=DIRECTION('',(0.,0.,1.));
#6293=DIRECTION('',(1.22464679914735E-16,1.,0.));
#6294=DIRECTION('',(0.,-0.888557159765256,-0.4587659248788));
#6295=DIRECTION('',(0.,-0.4587659248788,0.888557159765256));
#6296=DIRECTION('',(0.,-0.888557159765256,-0.4587659248788));
#6297=DIRECTION('',(0.,-0.4587659248788,0.888557159765256));
#6298=DIRECTION('',(0.,-0.888557159765258,-0.458765924878798));
#6299=DIRECTION('',(0.,-0.458765924878798,0.888557159765258));
#6300=DIRECTION('',(0.,-1.48882899694033E-16,1.));
#6301=DIRECTION('',(0.,-1.,-1.48882899694033E-16));
#6302=DIRECTION('',(0.,-0.897334135151735,0.441351843648));
#6303=DIRECTION('',(0.,0.441351843648,0.897334135151735));
#6304=DIRECTION('',(0.986273440214686,0.165120262618151,0.));
#6305=DIRECTION('',(0.165120262618151,-0.986273440214686,0.));
#6306=DIRECTION('',(0.986273440214687,0.165120262618151,-6.12323399573688E-17));
#6307=DIRECTION('',(-0.165120262618151,0.986273440214687,5.54312453933483E-14));
#6308=DIRECTION('',(-0.165120262618151,0.986273440214687,0.));
#6309=DIRECTION('',(0.,0.,1.));
#6310=DIRECTION('',(0.165120262618151,-0.986273440214686,0.));
#6311=DIRECTION('',(0.,0.,-1.));
#6312=DIRECTION('',(-0.143488198627506,0.85706379729923,0.494826014083392));
#6313=DIRECTION('',(0.,0.,1.));
#6314=DIRECTION('',(-1.,0.,0.));
#6315=DIRECTION('',(0.,0.,-1.));
#6316=DIRECTION('',(-0.986273440214686,0.165120262618152,0.));
#6317=DIRECTION('',(0.165120262618152,0.986273440214686,0.));
#6318=DIRECTION('',(0.165120262618152,0.986273440214686,0.));
#6319=DIRECTION('',(0.,7.9356111150447E-16,1.));
#6320=DIRECTION('',(-0.165120262618152,-0.986273440214686,0.));
#6321=DIRECTION('',(0.986273440214686,-0.165120262618152,6.12323399573693E-17));
#6322=DIRECTION('',(-0.165120262618152,-0.986273440214686,1.41223724344064E-13));
#6323=DIRECTION('',(0.143488198627506,0.85706379729923,0.494826014083392));
#6324=DIRECTION('',(0.,0.5,-0.866025403784439));
#6325=DIRECTION('',(0.,0.866025403784439,0.5));
#6326=DIRECTION('',(1.,0.,0.));
#6327=DIRECTION('',(0.,0.,1.));
#6328=DIRECTION('',(0.,-1.,0.));
#6329=DIRECTION('',(0.,0.,-1.));
#6330=DIRECTION('',(0.,-1.,0.));
#6331=DIRECTION('',(-1.,0.,0.));
#6332=DIRECTION('',(0.,0.,-1.));
#6333=DIRECTION('',(1.,0.,0.));
#6334=DIRECTION('',(0.,0.,-1.));
#6335=DIRECTION('',(-1.,0.,0.));
#6336=DIRECTION('',(0.,0.,1.));
#6337=DIRECTION('',(-0.986273440214685,0.16512026261816,0.));
#6338=DIRECTION('',(0.,0.,-1.));
#6339=DIRECTION('',(0.939132344209141,-0.343555585109954,0.));
#6340=DIRECTION('',(0.,0.,1.));
#6341=DIRECTION('',(0.939132344209136,-0.343555585109968,0.));
#6342=DIRECTION('',(0.,0.,-1.));
#6343=DIRECTION('',(0.939132344209141,-0.343555585109954,0.));
#6344=DIRECTION('',(0.,0.,1.));
#6345=DIRECTION('',(0.,0.,1.));
#6346=DIRECTION('',(0.,1.,0.));
#6347=DIRECTION('',(0.,0.,-1.));
#6348=DIRECTION('',(0.997579197588364,0.0695395178222898,0.));
#6349=DIRECTION('',(0.,0.,-1.));
#6350=DIRECTION('',(-1.,0.,0.));
#6351=DIRECTION('',(0.,0.,-1.));
#6352=DIRECTION('',(-0.965831339887311,0.259171416038655,0.));
#6353=DIRECTION('',(0.,0.,1.));
#6354=DIRECTION('',(0.,1.,0.));
#6355=DIRECTION('',(0.,0.,-1.));
#6356=DIRECTION('',(-0.986273440214686,0.165120262618152,0.));
#6357=DIRECTION('',(0.,0.,1.));
#6358=DIRECTION('',(0.,0.,1.));
#6359=DIRECTION('',(-1.,0.,0.));
#6360=DIRECTION('',(0.,-1.48882899694033E-16,1.));
#6361=DIRECTION('',(0.,-1.,-1.48882899694033E-16));
#6362=DIRECTION('',(0.,0.,-1.));
#6363=DIRECTION('',(-1.,0.,0.));
#6364=DIRECTION('',(0.,0.,1.));
#6365=DIRECTION('',(1.,0.,0.));
#6366=DIRECTION('',(0.,0.,1.));
#6367=DIRECTION('',(1.,0.,0.));
#6402=CARTESIAN_POINT('',(0.,0.,0.));
#8069=CARTESIAN_POINT('',(0.,0.04,-0.01475));
#8070=CARTESIAN_POINT('',(-3.5527136788005E-18,0.04,-0.01475));
#8071=CARTESIAN_POINT('',(-2.15430680055009E-18,0.016545,-0.01475));
#8072=CARTESIAN_POINT('',(0.,0.04,-0.013));
#8073=CARTESIAN_POINT('',(0.023455,0.04,-0.013));
#8074=CARTESIAN_POINT('',(0.,0.,0.03475));
#8075=CARTESIAN_POINT('',(0.,3.5527136788005E-18,0.03475));
#8076=CARTESIAN_POINT('',(0.,-0.031,0.03475));
#8077=CARTESIAN_POINT('',(-0.0306106219790423,0.00821406172744382,0.03475));
#8078=CARTESIAN_POINT('',(-0.0306106219790423,0.00821406172744363,0.03475));
#8079=CARTESIAN_POINT('',(-0.0316168242325797,0.00220395404948401,0.03475));
#8080=CARTESIAN_POINT('',(9.14113229555369E-15,3.31512595153072E-16,0.03475));
#8081=CARTESIAN_POINT('',(0.0316168242325797,0.00220395404948389,0.03475));
#8082=CARTESIAN_POINT('',(0.0316168242325796,0.00220395404948426,0.03475));
#8083=CARTESIAN_POINT('',(0.0306106219790423,0.00821406172744343,0.03475));
#8084=CARTESIAN_POINT('',(-3.5527136788005E-18,-2.41584530158434E-16,0.03475));
#8085=CARTESIAN_POINT('',(0.,0.04,-0.01475));
#8086=CARTESIAN_POINT('',(0.,0.04,0.013));
#8087=CARTESIAN_POINT('',(0.023455,0.04,0.013));
#8088=CARTESIAN_POINT('',(0.,0.04,0.01475));
#8089=CARTESIAN_POINT('',(-2.15430680055009E-18,0.016545,0.01475));
#8090=CARTESIAN_POINT('',(0.,0.,0.01475));
#8091=CARTESIAN_POINT('',(-0.0246568360053671,0.0437763899447745,0.01475));
#8092=CARTESIAN_POINT('',(-0.0246568360053672,0.0437763899447745,0.01475));
#8093=CARTESIAN_POINT('',(-0.0292158701188273,0.016545,0.01475));
#8094=CARTESIAN_POINT('',(0.,0.0396483833793207,0.01475));
#8095=CARTESIAN_POINT('',(0.0246568360053672,0.0437763899447744,0.01475));
#8096=CARTESIAN_POINT('',(0.0292158701188273,0.016545,0.01475));
#8097=CARTESIAN_POINT('',(0.0292158701188273,0.016545,0.01475));
#8098=CARTESIAN_POINT('',(0.,0.016545,0.01475));
#8099=CARTESIAN_POINT('',(-0.0292158701188273,0.016545,0.01475));
#8100=CARTESIAN_POINT('',(-0.0246568360053672,0.0437763899447744,0.01475));
#8101=CARTESIAN_POINT('',(-0.0378009992483934,-0.0347345020250511,0.03475));
#8102=CARTESIAN_POINT('',(-0.0378009992483934,-0.0347345020250511,0.023703850251217));
#8103=CARTESIAN_POINT('',(-0.0378009992483934,-0.0347345020250511,0.01475));
#8104=CARTESIAN_POINT('',(-0.0378009992483934,-0.0347345020250514,0.0237038502512178));
#8105=CARTESIAN_POINT('',(-0.0368117095543267,-0.028825414100497,0.0263618831657078));
#8106=CARTESIAN_POINT('',(-0.0353140091295469,-0.0198795577474549,0.0300968033298601));
#8107=CARTESIAN_POINT('',(-0.0332464653126233,-0.00752999191720053,0.0336219976537701));
#8108=CARTESIAN_POINT('',(-0.0321651420015115,-0.00107118156210252,0.0345704738450062));
#8109=CARTESIAN_POINT('',(-0.0316168242325796,0.00220395404948438,0.03475));
#8110=CARTESIAN_POINT('',(-0.0306106219790424,0.00821406172744319,0.03475));
#8111=CARTESIAN_POINT('',(-0.0295634232344042,0.0144690439572817,0.0344071339197969));
#8112=CARTESIAN_POINT('',(-0.0280531226089405,0.023490162080617,0.0323086955216529));
#8113=CARTESIAN_POINT('',(-0.0260933521506431,0.0351959910399979,0.0280191209876104));
#8114=CARTESIAN_POINT('',(-0.0251337005339458,0.0409280489134541,0.0255827730094403));
#8115=CARTESIAN_POINT('',(-0.0246568360053672,0.0437763899447744,0.0243187471298646));
#8116=CARTESIAN_POINT('',(-0.0246568360053672,0.0437763899447744,0.0243187471298645));
#8117=CARTESIAN_POINT('',(-0.0246568360053672,0.0437763899447744,0.01475));
#8118=CARTESIAN_POINT('',(-0.0292158701188273,0.016545,0.01475));
#8119=CARTESIAN_POINT('',(-0.0301785005652825,0.0107951493939822,0.0180696777951845));
#8120=CARTESIAN_POINT('',(-0.0328228982644232,-0.00500000000000008,9.74398446444435E-16));
#8121=CARTESIAN_POINT('',(-0.0359925369038936,-0.0239324456951552,0.01475));
#8122=CARTESIAN_POINT('',(-0.0359925369038936,-0.0239324456951552,0.01475));
#8123=CARTESIAN_POINT('',(0.,0.0396483833793206,0.01475));
#8124=CARTESIAN_POINT('',(0.0246568360053672,0.0437763899447744,0.01475));
#8125=CARTESIAN_POINT('',(0.0246568360053672,0.0437763899447744,0.0243187471298645));
#8126=CARTESIAN_POINT('',(0.0246568360053672,0.0437763899447744,0.0243187471298645));
#8127=CARTESIAN_POINT('',(0.0244261853211846,0.0451540806059303,0.0237073608419861));
#8128=CARTESIAN_POINT('',(0.0237401730081735,0.0478513323651511,0.0225495539156216));
#8129=CARTESIAN_POINT('',(0.0220160563070537,0.0517517948752077,0.0209652302526427));
#8130=CARTESIAN_POINT('',(0.0196049545771385,0.0553614641532363,0.0195673509638163));
#8131=CARTESIAN_POINT('',(0.017099633522645,0.0579907667344688,0.0185880719938733));
#8132=CARTESIAN_POINT('',(0.0147739750807182,0.0598569590563098,0.0179084194319801));
#8133=CARTESIAN_POINT('',(0.0123188659295968,0.0614896150378863,0.0173219949128185));
#8134=CARTESIAN_POINT('',(0.00963379108842836,0.0628045261969582,0.0168584228983841));
#8135=CARTESIAN_POINT('',(0.00675058877664492,0.0637552942897914,0.0165267592659007));
#8136=CARTESIAN_POINT('',(0.00455868160860307,0.0642632338451499,0.016350624923397));
#8137=CARTESIAN_POINT('',(0.00232530241794498,0.0645748845481871,0.0162429673551511));
#8138=CARTESIAN_POINT('',(-0.000730145584882101,0.0647186399709299,0.0161934340105266));
#8139=CARTESIAN_POINT('',(-0.00448154172001927,0.0643831294290258,0.0163089192735986));
#8140=CARTESIAN_POINT('',(-0.00889253724512921,0.063158749299646,0.0167337022307577));
#8141=CARTESIAN_POINT('',(-0.0129159464029183,0.0612090163507092,0.0174206501423198));
#8142=CARTESIAN_POINT('',(-0.0165490656269635,0.0585607841848676,0.018376082990071));
#8143=CARTESIAN_POINT('',(-0.019573225286212,0.0554035625895421,0.0195512513532641));
#8144=CARTESIAN_POINT('',(-0.0220017012360611,0.0517767203594562,0.0209554657275274));
#8145=CARTESIAN_POINT('',(-0.0237257985583774,0.0478972977786982,0.0225301676982113));
#8146=CARTESIAN_POINT('',(-0.02442605904778,0.0451548348447085,0.0237070261287883));
#8147=CARTESIAN_POINT('',(-0.0246568360053672,0.0437763899447744,0.0243187471298645));
#8148=CARTESIAN_POINT('',(0.0380113643198406,-0.035991025479093,0.01475));
#8149=CARTESIAN_POINT('',(0.0316168242325796,0.00220395404948427,0.03475));
#8150=CARTESIAN_POINT('',(0.0321613770800548,-0.00104869345568607,0.0345717065277884));
#8151=CARTESIAN_POINT('',(0.0332369380205949,-0.00747308481848439,0.0336336993032955));
#8152=CARTESIAN_POINT('',(0.0353058383379611,-0.0198307531089519,0.0301170420907904));
#8153=CARTESIAN_POINT('',(0.0368117177997724,-0.0288254633510492,0.0263618610117663));
#8154=CARTESIAN_POINT('',(0.0378009992483934,-0.0347345020250515,0.0237038502512177));
#8155=CARTESIAN_POINT('',(0.0378009992483934,-0.0347345020250512,0.023703850251217));
#8156=CARTESIAN_POINT('',(0.0378009992483934,-0.0347345020250512,0.03475));
#8157=CARTESIAN_POINT('',(0.0378009992483933,-0.0347345020250512,0.01475));
#8158=CARTESIAN_POINT('',(0.0378009992483934,-0.0347345020250512,0.01475));
#8159=CARTESIAN_POINT('',(0.0359925369038936,-0.0239324456951552,0.01475));
#8160=CARTESIAN_POINT('',(0.0328228982644231,-0.00499999999999992,-9.95936773122163E-16));
#8161=CARTESIAN_POINT('',(0.0301785005652825,0.0107951493939822,0.0180696777951845));
#8162=CARTESIAN_POINT('',(0.0292158701188273,0.016545,0.01475));
#8163=CARTESIAN_POINT('',(0.0246568360053672,0.0437763899447744,0.0243187471298645));
#8164=CARTESIAN_POINT('',(0.0256113237094467,0.0380751764376103,0.0268488098361206));
#8165=CARTESIAN_POINT('',(0.0275367186777366,0.0265746743851222,0.0315652051820333));
#8166=CARTESIAN_POINT('',(0.0295518358256032,0.0145382562596371,0.0344033400559715));
#8167=CARTESIAN_POINT('',(0.0306106219790424,0.00821406172744323,0.03475));
#8168=CARTESIAN_POINT('',(-0.0776088178345611,0.016545,0.01475));
#8169=CARTESIAN_POINT('',(-0.0301785005652825,0.0107951493939822,0.0180696777951845));
#8170=CARTESIAN_POINT('',(0.,0.04,-0.01175));
#8171=CARTESIAN_POINT('',(-0.00299951436620848,0.0628035723860738,-0.000162163751728459));
#8172=CARTESIAN_POINT('',(-0.00298616956258704,0.0628053277220141,-0.000995832260055065));
#8173=CARTESIAN_POINT('',(-0.00254014574668273,0.0628722334227876,-0.00223100782570009));
#8174=CARTESIAN_POINT('',(-0.00117231465122705,0.0629802629940287,-0.0032232282026831));
#8175=CARTESIAN_POINT('',(8.01521282900886E-5,0.0630117090883974,-0.00346781061358092));
#8176=CARTESIAN_POINT('',(0.00131266368591674,0.0629721307884194,-0.00315684322603784));
#8177=CARTESIAN_POINT('',(0.00263020704257935,0.0628607368680939,-0.00209512290266155));
#8178=CARTESIAN_POINT('',(0.00302049641875689,0.0628008132477051,-0.000835904596421582));
#8179=CARTESIAN_POINT('',(0.00299869834880741,0.0628036797077327,-1.91430325382278E-6));
#8180=CARTESIAN_POINT('',(-0.00301347071341734,0.0627996817593204,-0.000162387542955616));
#8181=CARTESIAN_POINT('',(0.00299869834880741,0.0628036797077327,-1.91430325382258E-6));
#8182=CARTESIAN_POINT('',(0.00299869834880741,0.0628036797077327,-1.91430325382263E-6));
#8183=CARTESIAN_POINT('',(0.00302130816342431,0.0628007065027663,0.000854614323236115));
#8184=CARTESIAN_POINT('',(0.00259825946404886,0.0628658285166061,0.00214294347958513));
#8185=CARTESIAN_POINT('',(0.00120652330326989,0.0629790253939967,0.00318205761014775));
#8186=CARTESIAN_POINT('',(-8.18799057279445E-5,0.0630123973788089,0.00343928974013122));
#8187=CARTESIAN_POINT('',(-0.00134744482602329,0.0629705900264957,0.0031137978980331));
#8188=CARTESIAN_POINT('',(-0.0026872335470843,0.0628541682503654,0.00200214986129947));
#8189=CARTESIAN_POINT('',(-0.00304999645721831,0.0627969525635701,0.000694293045094904));
#8190=CARTESIAN_POINT('',(-0.0029911325100996,0.062804673343572,-0.000160791461252475));
#8191=CARTESIAN_POINT('',(0.,0.04,-0.013));
#8192=CARTESIAN_POINT('',(0.023,0.04,-0.013));
#8193=CARTESIAN_POINT('',(0.,0.04,0.013));
#8194=CARTESIAN_POINT('',(0.023,0.04,0.013));
#8195=CARTESIAN_POINT('',(-0.0776088178345611,-0.005,0.));
#8196=CARTESIAN_POINT('',(-0.0359925369038936,-0.0239324456951552,0.01475));
#8197=CARTESIAN_POINT('',(0.,0.,0.01475));
#8198=CARTESIAN_POINT('',(0.0328696320473201,-0.0355601033381419,0.01475));
#8199=CARTESIAN_POINT('',(0.0375652937683657,-0.0372778812636918,0.01475));
#8200=CARTESIAN_POINT('',(0.,-0.0235356578592935,0.01475));
#8201=CARTESIAN_POINT('',(-0.0375652937683657,-0.0372778812636917,0.01475));
#8202=CARTESIAN_POINT('',(-0.0328696320473199,-0.0355601033381419,0.01475));
#8203=CARTESIAN_POINT('',(-0.0328696320473199,-0.0355601033381419,0.6722362));
#8204=CARTESIAN_POINT('',(-0.0378009992483934,-0.0347345020250511,0.023703850251217));
#8205=CARTESIAN_POINT('',(-0.0379395336899237,-0.0355619767278518,0.0233316346023665));
#8206=CARTESIAN_POINT('',(-0.037872659461892,-0.0364376764269736,0.0230218844628341));
#8207=CARTESIAN_POINT('',(-0.0375652937683657,-0.0372778812636916,0.0228117569919867));
#8208=CARTESIAN_POINT('',(-0.0375652937683657,-0.0372778812636917,0.0228117569919868));
#8209=CARTESIAN_POINT('',(-0.0375652937683657,-0.0372778812636917,0.03475));
#8210=CARTESIAN_POINT('',(0.,0.,0.052010716339737));
#8211=CARTESIAN_POINT('',(-0.0375652937683657,-0.0372778812636917,0.0228117569919867));
#8212=CARTESIAN_POINT('',(-0.0368723820726594,-0.039172002079426,0.0223380548671046));
#8213=CARTESIAN_POINT('',(-0.0352157180117104,-0.0428159221045996,0.0214491533403092));
#8214=CARTESIAN_POINT('',(-0.0319460092255036,-0.0478638720648067,0.0202662014447962));
#8215=CARTESIAN_POINT('',(-0.0278553048475434,-0.0524566122744212,0.0192266496656653));
#8216=CARTESIAN_POINT('',(-0.0231991299966274,-0.0563114964548188,0.018378556689204));
#8217=CARTESIAN_POINT('',(-0.0178753310411592,-0.0594966216850981,0.017693286407371));
#8218=CARTESIAN_POINT('',(-0.0131542346956908,-0.0614064131407065,0.0172893487407261));
#8219=CARTESIAN_POINT('',(-0.00921290916609484,-0.0625013441622402,0.017059391860532));
#8220=CARTESIAN_POINT('',(-0.00514084969644836,-0.0632982746320762,0.0168927558921429));
#8221=CARTESIAN_POINT('',(-0.00105859844217804,-0.0636123136064291,0.0168274299026073));
#8222=CARTESIAN_POINT('',(0.00302765394536762,-0.0634608055949469,0.0168589666787993));
#8223=CARTESIAN_POINT('',(0.00714179578061486,-0.0629880118531215,0.0169575656489395));
#8224=CARTESIAN_POINT('',(0.012138786389917,-0.0618126013351542,0.0172034657543907));
#8225=CARTESIAN_POINT('',(0.0168785934868732,-0.0599024129561901,0.0176074426371329));
#8226=CARTESIAN_POINT('',(0.0205024280655964,-0.0579276333929854,0.018030809406638));
#8227=CARTESIAN_POINT('',(0.0239104204872156,-0.0557140964769394,0.0185100961237082));
#8228=CARTESIAN_POINT('',(0.0278285765558024,-0.052485794077695,0.0192200913642277));
#8229=CARTESIAN_POINT('',(0.0319146778455702,-0.0479016398645519,0.0202576003571143));
#8230=CARTESIAN_POINT('',(0.0351896104969302,-0.042869047811016,0.021436316620234));
#8231=CARTESIAN_POINT('',(0.036872298394842,-0.039172230818379,0.0223379976616047));
#8232=CARTESIAN_POINT('',(0.0375652937683656,-0.0372778812636917,0.0228117569919867));
#8233=CARTESIAN_POINT('',(0.0375652937683657,-0.0372778812636918,0.0228117569919868));
#8234=CARTESIAN_POINT('',(0.0375652937683657,-0.0372778812636917,0.0228117569919867));
#8235=CARTESIAN_POINT('',(0.0378729252083338,-0.0364369499911663,0.0230220661377213));
#8236=CARTESIAN_POINT('',(0.0379396433028291,-0.0355626314524483,0.0233313400933747));
#8237=CARTESIAN_POINT('',(0.0378009992483934,-0.0347345020250512,0.023703850251217));
#8238=CARTESIAN_POINT('',(0.,0.,0.052010716339737));
#8239=CARTESIAN_POINT('',(0.0328696320473199,-0.0355601033381419,0.6722362));
#8240=CARTESIAN_POINT('',(0.0375652937683657,-0.0372778812636918,0.03475));
#8241=CARTESIAN_POINT('',(0.,-0.042724949124795,-0.0545862509068234));
#8242=CARTESIAN_POINT('',(-9.60170206471803E-16,0.0629999999999978,-6.68354260824344E-17));
#8243=CARTESIAN_POINT('',(8.09786277180737E-17,-0.0290000000000004,-0.0475));
#8244=CARTESIAN_POINT('',(-0.0029997619807752,-0.028844434958215,-0.0474622103361266));
#8245=CARTESIAN_POINT('',(0.0029997619807752,-0.028844434958215,-0.0474622103361266));
#8246=CARTESIAN_POINT('',(-0.0029997619807752,-0.028844434958215,-0.0474622103361266));
#8247=CARTESIAN_POINT('',(-0.00300915492826778,-0.0288434581109716,-0.0466225739694568));
#8248=CARTESIAN_POINT('',(-0.00259693992861547,-0.0288930415527731,-0.0453675967135918));
#8249=CARTESIAN_POINT('',(-0.00125704785411636,-0.0289806255271393,-0.0443171156875614));
#8250=CARTESIAN_POINT('',(-4.87566413189158E-6,-0.0290095691748998,-0.0440282561890832));
#8251=CARTESIAN_POINT('',(0.00124683950271356,-0.0289810952366406,-0.0443123258170411));
#8252=CARTESIAN_POINT('',(0.00259350062251134,-0.0288934852584709,-0.0453594477105172));
#8253=CARTESIAN_POINT('',(0.0030091625757541,-0.0288434573156488,-0.0466218903600113));
#8254=CARTESIAN_POINT('',(0.0029997619807752,-0.028844434958215,-0.0474622103361266));
#8255=CARTESIAN_POINT('',(0.,-0.029,0.04525));
#8256=CARTESIAN_POINT('',(1.57973819895899E-16,-0.0289999999999994,0.04525));
#8257=CARTESIAN_POINT('',(-0.00299978173590996,-0.0288444329037148,0.0452138124758919));
#8258=CARTESIAN_POINT('',(0.00299978173590995,-0.0288444329037148,0.0452138124758922));
#8259=CARTESIAN_POINT('',(0.00299978173590995,-0.0288444329037148,0.0452138124758922));
#8260=CARTESIAN_POINT('',(0.00300881962437,-0.0288434929756245,0.0443784326540771));
#8261=CARTESIAN_POINT('',(0.00259047495675581,-0.0288936910635023,0.0431307616648426));
#8262=CARTESIAN_POINT('',(0.00125009688665756,-0.0289808842450609,0.0420961922125352));
#8263=CARTESIAN_POINT('',(4.15924442233007E-6,-0.0290094521029003,0.0418131179333976));
#8264=CARTESIAN_POINT('',(-0.00124075947786621,-0.0289813054046344,0.0420919385455001));
#8265=CARTESIAN_POINT('',(-0.00258736867356594,-0.0288940972630226,0.0431234114486747));
#8266=CARTESIAN_POINT('',(-0.00300882587110642,-0.0288434923259724,0.0443778552628386));
#8267=CARTESIAN_POINT('',(-0.00299978173590996,-0.0288444329037148,0.0452138124758919));
#8268=CARTESIAN_POINT('',(0.,-0.0235356578592935,0.01475));
#8269=CARTESIAN_POINT('',(0.,0.,0.040025));
#8270=CARTESIAN_POINT('',(-1.77635683940025E-18,-1.77635683940025E-18,0.03525));
#8271=CARTESIAN_POINT('',(-3.85185988877447E-34,0.031,0.03525));
#8272=CARTESIAN_POINT('',(0.,0.,-0.03475));
#8273=CARTESIAN_POINT('',(0.,0.,-0.0582267070030276));
#8274=CARTESIAN_POINT('',(0.,-0.029,-0.0582267070030276));
#8275=CARTESIAN_POINT('',(0.,-1.77635683940025E-18,-0.03525));
#8276=CARTESIAN_POINT('',(-0.029,-7.10295143505464E-18,-0.03525));
#8277=CARTESIAN_POINT('',(-3.04987242545569E-5,-0.0291479853908251,-0.0474999612573823));
#8278=CARTESIAN_POINT('',(-0.00293657158878645,-0.0288509366798365,-0.0481136345035384));
#8279=CARTESIAN_POINT('',(3.05022327937685E-5,-0.0291479966421305,-0.047499961485425));
#8280=CARTESIAN_POINT('',(0.00293657158878639,-0.0288509366798365,-0.0481136345035382));
#8281=CARTESIAN_POINT('',(0.00293657158878639,-0.0288509366798365,-0.0481136345035382));
#8282=CARTESIAN_POINT('',(0.00280389719458576,-0.0288644408464738,-0.0488351566656889));
#8283=CARTESIAN_POINT('',(0.00230583590197879,-0.0289167653919492,-0.0498467610228945));
#8284=CARTESIAN_POINT('',(0.00109971947815042,-0.0289851551437462,-0.0507117731397796));
#8285=CARTESIAN_POINT('',(1.04397156723601E-5,-0.0290072736075878,-0.0509568367298539));
#8286=CARTESIAN_POINT('',(-0.00108651055265419,-0.0289857417435524,-0.0507183410275081));
#8287=CARTESIAN_POINT('',(-0.00229752899548612,-0.0289175088319034,-0.0498589259558951));
#8288=CARTESIAN_POINT('',(-0.0028037279324821,-0.0288644580746938,-0.0488360771625165));
#8289=CARTESIAN_POINT('',(-0.00293657158878634,-0.0288509366798365,-0.0481136345035385));
#8290=CARTESIAN_POINT('',(3.04866257696342E-5,0.029147946587811,-0.0475000395289292));
#8291=CARTESIAN_POINT('',(0.00299976198077498,0.0288444349582151,-0.0475377896638955));
#8292=CARTESIAN_POINT('',(0.00293657158878635,0.0288509366798365,-0.0468863654964615));
#8293=CARTESIAN_POINT('',(0.00293657158878637,0.0288509366798365,-0.0468863654964617));
#8294=CARTESIAN_POINT('',(0.00280389719458545,0.0288644408464739,-0.0461648433343095));
#8295=CARTESIAN_POINT('',(0.00230583590197662,0.0289167653919494,-0.0451532389771017));
#8296=CARTESIAN_POINT('',(0.00109971947814396,0.0289851551437465,-0.044288226860217));
#8297=CARTESIAN_POINT('',(1.04397156625072E-5,0.0290072736075879,-0.0440431632701459));
#8298=CARTESIAN_POINT('',(-0.00108651055266498,0.028985741743552,-0.0442816589724958));
#8299=CARTESIAN_POINT('',(-0.00229752899549738,0.0289175088319024,-0.0451410740441204));
#8300=CARTESIAN_POINT('',(-0.00280372793248197,0.0288644580746939,-0.0461639228374824));
#8301=CARTESIAN_POINT('',(-0.00293657158878641,0.0288509366798365,-0.0468863654964619));
#8302=CARTESIAN_POINT('',(-0.00293657158879015,0.0288509366798361,-0.0468863654964798));
#8303=CARTESIAN_POINT('',(-3.0487773813507E-5,0.0291479502701906,-0.0475000394543178));
#8304=CARTESIAN_POINT('',(-0.00299976198077519,0.028844434958215,-0.0475377896638737));
#8305=CARTESIAN_POINT('',(-0.00299976198077519,0.028844434958215,-0.0475377896638734));
#8306=CARTESIAN_POINT('',(-0.00300915492826783,0.0288434581109716,-0.0483774260305414));
#8307=CARTESIAN_POINT('',(-0.00259693992861748,0.0288930415527728,-0.0496324032864039));
#8308=CARTESIAN_POINT('',(-0.00125704785412371,0.028980625527139,-0.0506828843124349));
#8309=CARTESIAN_POINT('',(-4.8756641433718E-6,0.0290095691748998,-0.050971743810917));
#8310=CARTESIAN_POINT('',(0.00124683950270104,0.0289810952366412,-0.050687674182964));
#8311=CARTESIAN_POINT('',(0.00259350062249991,0.028893485258472,-0.0496405522895028));
#8312=CARTESIAN_POINT('',(0.00300916257575402,0.0288434573156488,-0.0483781096399874));
#8313=CARTESIAN_POINT('',(0.0029997619807752,0.028844434958215,-0.047537789663874));
#8314=CARTESIAN_POINT('',(0.,-0.029,-0.0475));
#8315=CARTESIAN_POINT('',(0.,0.029,-0.0475));
#8316=CARTESIAN_POINT('',(5.25708289276628E-16,0.0290000000000022,-0.0475));
#8317=CARTESIAN_POINT('',(0.,-0.029,-0.0475));
#8318=CARTESIAN_POINT('',(0.,0.,0.03475));
#8319=CARTESIAN_POINT('',(0.,0.,0.05475));
#8320=CARTESIAN_POINT('',(-0.029,0.,0.05475));
#8321=CARTESIAN_POINT('',(0.,-1.77635683940025E-18,0.03525));
#8322=CARTESIAN_POINT('',(0.029,-7.10295143505464E-18,0.03525));
#8323=CARTESIAN_POINT('',(0.00293126735069296,-0.028851476075216,0.0458884917530881));
#8324=CARTESIAN_POINT('',(0.00297968219936272,-0.0288465571981081,0.0456662228443543));
#8325=CARTESIAN_POINT('',(0.00300252637978852,-0.0288441474644896,0.0454413310138827));
#8326=CARTESIAN_POINT('',(0.00299978173590996,-0.0288444329037148,0.0452138124758922));
#8327=CARTESIAN_POINT('',(0.00293126735069295,-0.028851476075216,0.0458884917530881));
#8328=CARTESIAN_POINT('',(-3.03426997834468E-5,-0.0291474821613309,0.0452499544771244));
#8329=CARTESIAN_POINT('',(-0.00293126735069299,-0.028851476075216,0.045888491753088));
#8330=CARTESIAN_POINT('',(-0.00293126735069298,-0.028851476075216,0.045888491753088));
#8331=CARTESIAN_POINT('',(-0.00279340273508677,-0.0288654829165121,0.0466007213942467));
#8332=CARTESIAN_POINT('',(-0.00228610200596045,-0.0289182971695779,0.0475964784080196));
#8333=CARTESIAN_POINT('',(-0.0010888098504506,-0.028985444454822,0.0484335917950664));
#8334=CARTESIAN_POINT('',(-1.20064574058231E-5,-0.029007083304106,0.0486708430585802));
#8335=CARTESIAN_POINT('',(0.00107164560000882,-0.0289862101168382,0.0484423158488964));
#8336=CARTESIAN_POINT('',(0.00228223772074259,-0.0289187855098398,0.0476048968650648));
#8337=CARTESIAN_POINT('',(0.00279317831835183,-0.0288655057169208,0.0466018807653434));
#8338=CARTESIAN_POINT('',(0.00293126735069296,-0.028851476075216,0.0458884917530881));
#8339=CARTESIAN_POINT('',(-0.00235329472491155,0.0289222292213958,0.0429007124101602));
#8340=CARTESIAN_POINT('',(5.94732789712727E-7,0.0290388471998873,0.0419247819883626));
#8341=CARTESIAN_POINT('',(0.00235091579375268,0.0289223819790551,0.0429001596363893));
#8342=CARTESIAN_POINT('',(0.00332394666285095,0.0288054625306398,0.0452469399202865));
#8343=CARTESIAN_POINT('',(0.00235329301180312,0.0289222295931621,0.0475992920377153));
#8344=CARTESIAN_POINT('',(-6.06452073458359E-7,0.0290388471987158,0.0485752179920553));
#8345=CARTESIAN_POINT('',(-0.00235091745396515,0.0289223816119677,0.0475998359939933));
#8346=CARTESIAN_POINT('',(-0.00332394581952071,0.0288054627153532,0.0452530600601599));
#8347=CARTESIAN_POINT('',(-0.00235329472491155,0.0289222292213958,0.0429007124101602));
#8348=CARTESIAN_POINT('',(5.94732789712727E-7,0.0290388471998873,0.0419247819883626));
#8349=CARTESIAN_POINT('',(0.00235091579375268,0.0289223819790551,0.0429001596363893));
#8350=CARTESIAN_POINT('',(-2.98657244279343E-18,0.029,0.04225));
#8351=CARTESIAN_POINT('',(0.,-0.029,0.04525));
#8352=CARTESIAN_POINT('',(0.,-0.029,0.04525));
#8353=CARTESIAN_POINT('',(0.,0.,0.03525));
#8354=CARTESIAN_POINT('',(0.,0.,-0.01475));
#8355=CARTESIAN_POINT('',(0.0292158701188273,0.016545,-0.01475));
#8356=CARTESIAN_POINT('',(0.0292158701188273,0.016545,-0.01475));
#8357=CARTESIAN_POINT('',(0.0246568360053672,0.0437763899447744,-0.01475));
#8358=CARTESIAN_POINT('',(-1.77635683940025E-18,0.0396483833793206,-0.01475));
#8359=CARTESIAN_POINT('',(-0.0246568360053672,0.0437763899447744,-0.01475));
#8360=CARTESIAN_POINT('',(-0.0246568360053672,0.0437763899447744,-0.01475));
#8361=CARTESIAN_POINT('',(-0.0292158701188273,0.016545,-0.01475));
#8362=CARTESIAN_POINT('',(0.,0.016545,-0.01475));
#8363=CARTESIAN_POINT('',(0.0292158701188272,0.016545,-0.01475));
#8364=CARTESIAN_POINT('',(0.,0.,-0.03525));
#8365=CARTESIAN_POINT('',(0.,-1.77635683940025E-18,-0.03525));
#8366=CARTESIAN_POINT('',(3.79640507735679E-18,0.031,-0.03525));
#8367=CARTESIAN_POINT('',(0.,-0.029,-0.0475));
#8368=CARTESIAN_POINT('',(0.,0.029,-0.0475));
#8369=CARTESIAN_POINT('',(0.,-0.0791723446654833,-0.103349851865331));
#8370=CARTESIAN_POINT('',(0.,0.00822406222571555,-0.0582267070030276));
#8371=CARTESIAN_POINT('',(0.,0.00168477969117994,-0.0582267070030276));
#8372=CARTESIAN_POINT('',(0.,-0.047070468643187,0.054137920718524));
#8373=CARTESIAN_POINT('',(0.0246568360053672,0.0437763899447744,-0.01475));
#8374=CARTESIAN_POINT('',(0.0328228982644231,-0.005,2.50977123598683E-16));
#8375=CARTESIAN_POINT('',(0.0359925369038936,-0.0239324456951552,-0.01475));
#8376=CARTESIAN_POINT('',(0.0301785005652825,0.0107951493939822,-0.0180696777951845));
#8377=CARTESIAN_POINT('',(0.0378009992483933,-0.0347345020250512,-0.01475));
#8378=CARTESIAN_POINT('',(0.0378009992483933,-0.0347345020250512,-0.01475));
#8379=CARTESIAN_POINT('',(0.0378009992483933,-0.0347345020250512,-0.0237038502512179));
#8380=CARTESIAN_POINT('',(0.0378009992483934,-0.0347345020250516,-0.0237038502512177));
#8381=CARTESIAN_POINT('',(0.0316168242325796,0.00220395404948403,-0.03475));
#8382=CARTESIAN_POINT('',(0.0327062789897151,-0.00430342593066477,-0.0343932987682137));
#8383=CARTESIAN_POINT('',(0.034275406372161,-0.0136759198758738,-0.0321451100959277));
#8384=CARTESIAN_POINT('',(0.0363102609424209,-0.0258302308339899,-0.0276010341206553));
#8385=CARTESIAN_POINT('',(0.0373060148884253,-0.0317779301312242,-0.0250337789150296));
#8386=CARTESIAN_POINT('',(0.0378009992483935,-0.0347345020250519,-0.0237038502512176));
#8387=CARTESIAN_POINT('',(0.0316168242325797,0.0022039540494836,-0.03475));
#8388=CARTESIAN_POINT('',(0.0306106219790425,0.00821406172744211,-0.03475));
#8389=CARTESIAN_POINT('',(0.0306106219790424,0.008214061727443,-0.03475));
#8390=CARTESIAN_POINT('',(0.0246568360053671,0.0437763899447746,-0.0243187471298645));
#8391=CARTESIAN_POINT('',(0.0256113237094466,0.0380751764376104,-0.0268488098361205));
#8392=CARTESIAN_POINT('',(0.0275367186777367,0.0265746743851218,-0.0315652051820334));
#8393=CARTESIAN_POINT('',(0.0295518358256032,0.0145382562596374,-0.0344033400559715));
#8394=CARTESIAN_POINT('',(0.0306106219790423,0.00821406172744344,-0.03475));
#8395=CARTESIAN_POINT('',(0.0246568360053672,0.0437763899447745,-0.0243187471298645));
#8396=CARTESIAN_POINT('',(0.0246568360053672,0.0437763899447744,-0.01475));
#8397=CARTESIAN_POINT('',(0.0301785005652825,0.0107951493939822,-0.0180696777951845));
#8398=CARTESIAN_POINT('',(0.,0.0396483833793206,-0.01475));
#8399=CARTESIAN_POINT('',(-0.0246568360053672,0.0437763899447744,-0.01475));
#8400=CARTESIAN_POINT('',(-0.0246568360053672,0.0437763899447744,-0.0243187471298645));
#8401=CARTESIAN_POINT('',(0.0246568360053672,0.0437763899447746,-0.0243187471298645));
#8402=CARTESIAN_POINT('',(0.0244261853211846,0.0451540806059305,-0.023707360841986));
#8403=CARTESIAN_POINT('',(0.0237401730081734,0.0478513323651514,-0.0225495539156214));
#8404=CARTESIAN_POINT('',(0.0220160563070535,0.0517517948752079,-0.0209652302526425));
#8405=CARTESIAN_POINT('',(0.0196049545771384,0.0553614641532365,-0.0195673509638162));
#8406=CARTESIAN_POINT('',(0.0170996335226448,0.057990766734469,-0.0185880719938732));
#8407=CARTESIAN_POINT('',(0.014773975080718,0.0598569590563099,-0.01790841943198));
#8408=CARTESIAN_POINT('',(0.0123188659295966,0.0614896150378864,-0.0173219949128184));
#8409=CARTESIAN_POINT('',(0.00963379108842817,0.0628045261969582,-0.016858422898384));
#8410=CARTESIAN_POINT('',(0.00675058877664476,0.0637552942897915,-0.0165267592659006));
#8411=CARTESIAN_POINT('',(0.00455868160860291,0.0642632338451499,-0.016350624923397));
#8412=CARTESIAN_POINT('',(0.00232530241794481,0.0645748845481871,-0.0162429673551511));
#8413=CARTESIAN_POINT('',(-0.000730145584882256,0.0647186399709299,-0.0161934340105266));
#8414=CARTESIAN_POINT('',(-0.00448154172001943,0.0643831294290258,-0.0163089192735985));
#8415=CARTESIAN_POINT('',(-0.00889253724512927,0.063158749299646,-0.0167337022307577));
#8416=CARTESIAN_POINT('',(-0.0129159464029183,0.0612090163507091,-0.0174206501423198));
#8417=CARTESIAN_POINT('',(-0.0165490656269636,0.0585607841848676,-0.018376082990071));
#8418=CARTESIAN_POINT('',(-0.019573225286212,0.0554035625895421,-0.0195512513532641));
#8419=CARTESIAN_POINT('',(-0.0220017012360611,0.0517767203594562,-0.0209554657275274));
#8420=CARTESIAN_POINT('',(-0.0237257985583774,0.0478972977786982,-0.0225301676982113));
#8421=CARTESIAN_POINT('',(-0.02442605904778,0.0451548348447085,-0.0237070261287883));
#8422=CARTESIAN_POINT('',(-0.0246568360053672,0.0437763899447745,-0.0243187471298645));
#8423=CARTESIAN_POINT('',(-0.0380113643198406,-0.035991025479093,-0.01475));
#8424=CARTESIAN_POINT('',(-0.0306106219790426,0.00821406172744194,-0.03475));
#8425=CARTESIAN_POINT('',(-0.0295634232344044,0.0144690439572807,-0.0344071339197971));
#8426=CARTESIAN_POINT('',(-0.0280531226089406,0.0234901620806161,-0.0323086955216532));
#8427=CARTESIAN_POINT('',(-0.0260933521506431,0.0351959910399975,-0.0280191209876106));
#8428=CARTESIAN_POINT('',(-0.0251337005339458,0.0409280489134541,-0.0255827730094403));
#8429=CARTESIAN_POINT('',(-0.0246568360053671,0.0437763899447745,-0.0243187471298645));
#8430=CARTESIAN_POINT('',(-0.0306106219790425,0.00821406172744216,-0.03475));
#8431=CARTESIAN_POINT('',(-0.0316168242325796,0.00220395404948424,-0.03475));
#8432=CARTESIAN_POINT('',(-0.0316168242325796,0.00220395404948406,-0.03475));
#8433=CARTESIAN_POINT('',(-0.0378009992482983,-0.0347345020242971,-0.0237038502515795));
#8434=CARTESIAN_POINT('',(-0.0368102789739022,-0.02881686915583,-0.0263657268628202));
#8435=CARTESIAN_POINT('',(-0.0348121591335525,-0.0168819769893,-0.03134699023701));
#8436=CARTESIAN_POINT('',(-0.0327195944738099,-0.00438296013257355,-0.0343889391107361));
#8437=CARTESIAN_POINT('',(-0.0316168242325796,0.00220395404948413,-0.03475));
#8438=CARTESIAN_POINT('',(-0.0378009992483299,-0.0347345020246722,-0.0237038502513883));
#8439=CARTESIAN_POINT('',(-0.0378009992483934,-0.0347345020250511,-0.0237038502512179));
#8440=CARTESIAN_POINT('',(-0.0378009992483934,-0.0347345020250511,-0.01475));
#8441=CARTESIAN_POINT('',(-0.0359925369038936,-0.0239324456951552,-0.01475));
#8442=CARTESIAN_POINT('',(-0.0359925369038936,-0.0239324456951552,-0.01475));
#8443=CARTESIAN_POINT('',(-0.0328228982644232,-0.00500000000000008,-2.87703087949443E-16));
#8444=CARTESIAN_POINT('',(-0.0301785005652825,0.0107951493939822,-0.0180696777951845));
#8445=CARTESIAN_POINT('',(-0.0301785005652825,0.0107951493939822,-0.0180696777951845));
#8446=CARTESIAN_POINT('',(-0.0776088178345611,0.0078847459621556,-0.01975));
#8447=CARTESIAN_POINT('',(-0.0301785005652825,0.0107951493939822,-0.0180696777951845));
#8448=CARTESIAN_POINT('',(0.,0.,0.040025));
#8449=CARTESIAN_POINT('',(0.,3.5527136788005E-18,-0.03475));
#8450=CARTESIAN_POINT('',(0.,-0.031,-0.03475));
#8451=CARTESIAN_POINT('',(-0.0776088178345611,-0.005,0.));
#8452=CARTESIAN_POINT('',(-0.0359925369038936,-0.0239324456951552,-0.01475));
#8453=CARTESIAN_POINT('',(0.,0.,-0.01475));
#8454=CARTESIAN_POINT('',(-0.03286963204732,-0.0355601033381419,-0.01475));
#8455=CARTESIAN_POINT('',(-0.0375652937683657,-0.0372778812636917,-0.01475));
#8456=CARTESIAN_POINT('',(3.5527136788005E-18,-0.0235356578592935,-0.01475));
#8457=CARTESIAN_POINT('',(0.0375652937683657,-0.0372778812636918,-0.01475));
#8458=CARTESIAN_POINT('',(0.0328696320473203,-0.035560103338142,-0.01475));
#8459=CARTESIAN_POINT('',(0.0328696320473199,-0.0355601033381419,-0.77707293494511));
#8460=CARTESIAN_POINT('',(0.0375652937683657,-0.0372778812636918,-0.0228117569919877));
#8461=CARTESIAN_POINT('',(0.0375652937683657,-0.0372778812636918,-0.0228117569919877));
#8462=CARTESIAN_POINT('',(0.0378009992483935,-0.0347345020250519,-0.0237038502512175));
#8463=CARTESIAN_POINT('',(0.0379395343785947,-0.0355619808413266,-0.0233316327520394));
#8464=CARTESIAN_POINT('',(0.0378726603922854,-0.0364376738836806,-0.0230218850988891));
#8465=CARTESIAN_POINT('',(0.0375652937683657,-0.0372778812636918,-0.0228117569919877));
#8466=CARTESIAN_POINT('',(0.,0.,-0.052010716339737));
#8467=CARTESIAN_POINT('',(1.77635683940025E-18,5.32907051820075E-18,-0.03475));
#8468=CARTESIAN_POINT('',(-0.0375652937683657,-0.0372778812636917,-0.0228117569919877));
#8469=CARTESIAN_POINT('',(-0.0368723814300125,-0.0391720038361446,-0.0223380544277665));
#8470=CARTESIAN_POINT('',(-0.0352157157828944,-0.0428159259480469,-0.0214491524280103));
#8471=CARTESIAN_POINT('',(-0.0319460093286459,-0.0478638717967643,-0.0202662015107985));
#8472=CARTESIAN_POINT('',(-0.0278553031209884,-0.052456614149853,-0.0192266492426356));
#8473=CARTESIAN_POINT('',(-0.0231991281117714,-0.0563114975962444,-0.0183785564441856));
#8474=CARTESIAN_POINT('',(-0.0178753309559553,-0.0594966218536073,-0.0176932863706357));
#8475=CARTESIAN_POINT('',(-0.013154231246997,-0.0614064142875746,-0.0172893484991303));
#8476=CARTESIAN_POINT('',(-0.00921290864977878,-0.0625013442143116,-0.0170593918498272));
#8477=CARTESIAN_POINT('',(-0.0051408499180295,-0.0632982746670183,-0.0168927558847434));
#8478=CARTESIAN_POINT('',(-0.00105859515404703,-0.0636123137459811,-0.0168274298734829));
#8479=CARTESIAN_POINT('',(0.00302765575771894,-0.0634608053488871,-0.0168589667301854));
#8480=CARTESIAN_POINT('',(0.00714179333735995,-0.0629880122993201,-0.01695756555541));
#8481=CARTESIAN_POINT('',(0.0121387916213171,-0.0618125997379239,-0.0172034660910362));
#8482=CARTESIAN_POINT('',(0.0168785920660817,-0.0599024135514785,-0.0176074425106158));
#8483=CARTESIAN_POINT('',(0.0205024292275728,-0.0579276328140605,-0.0180308095300653));
#8484=CARTESIAN_POINT('',(0.0239104231105815,-0.0557140944842808,-0.0185100965594511));
#8485=CARTESIAN_POINT('',(0.0278285759269693,-0.0524857946247409,-0.0192200912425152));
#8486=CARTESIAN_POINT('',(0.031914679755287,-0.0479016376111136,-0.0202576008698634));
#8487=CARTESIAN_POINT('',(0.0351896110741646,-0.042869046351534,-0.0214363169788631));
#8488=CARTESIAN_POINT('',(0.0368722982470235,-0.0391722312224509,-0.022337997560551));
#8489=CARTESIAN_POINT('',(0.0375652937683657,-0.0372778812636918,-0.0228117569919877));
#8490=CARTESIAN_POINT('',(-0.0375652937683657,-0.0372778812636917,-0.0228117569919877));
#8491=CARTESIAN_POINT('',(-0.0375652937683657,-0.0372778812636917,-0.0228117569919877));
#8492=CARTESIAN_POINT('',(-0.0378729272452308,-0.0364369444231711,-0.0230220675302264));
#8493=CARTESIAN_POINT('',(-0.0379396435855259,-0.0355626331402284,-0.0233313393341246));
#8494=CARTESIAN_POINT('',(-0.0378009992482659,-0.0347345020242895,-0.0237038502515605));
#8495=CARTESIAN_POINT('',(0.,0.,-0.03475));
#8496=CARTESIAN_POINT('',(-3.5527136788005E-18,1.06581410364015E-17,-0.03475));
#8497=CARTESIAN_POINT('',(0.,0.,-0.052010716339737));
#8498=CARTESIAN_POINT('',(-0.0328696320473199,-0.0355601033381419,-0.77666486957853));
#8499=CARTESIAN_POINT('',(-0.0375652937683657,-0.0372778812636917,-0.0228117569919877));
#8500=CARTESIAN_POINT('',(0.,-0.0235356578592935,-0.01475));
#8501=CARTESIAN_POINT('',(-0.715243651719731,-0.0114123038947582,-0.0582267070030276));
#8502=CARTESIAN_POINT('',(-0.715243651719731,0.027040170002071,0.05475));
#8503=CARTESIAN_POINT('',(0.,0.04,-0.013));
#8504=CARTESIAN_POINT('',(0.,0.04,0.013));
#8534=MECHANICAL_DESIGN_GEOMETRIC_PRESENTATION_REPRESENTATION('',(#4343),#8535);
#8535=(
GEOMETRIC_REPRESENTATION_CONTEXT(3)
GLOBAL_UNCERTAINTY_ASSIGNED_CONTEXT((#8547))
GLOBAL_UNIT_ASSIGNED_CONTEXT((#8561,#8560,#8559))
REPRESENTATION_CONTEXT('MAS-680','TOP_LEVEL_ASSEMBLY_PART')
);
#8545=(
GEOMETRIC_REPRESENTATION_CONTEXT(3)
GLOBAL_UNCERTAINTY_ASSIGNED_CONTEXT((#8557))
GLOBAL_UNIT_ASSIGNED_CONTEXT((#8561,#8560,#8559))
REPRESENTATION_CONTEXT('CRANKSHAFT','COMPONENT_PART')
);
#8547=UNCERTAINTY_MEASURE_WITH_UNIT(LENGTH_MEASURE(1.E-8),#8561,
'DISTANCE_ACCURACY_VALUE','Maximum Tolerance applied to model');
#8557=UNCERTAINTY_MEASURE_WITH_UNIT(LENGTH_MEASURE(0.0002),#8561,
'DISTANCE_ACCURACY_VALUE','Maximum Tolerance applied to model');
#8559=(
NAMED_UNIT(*)
SI_UNIT($,.STERADIAN.)
SOLID_ANGLE_UNIT()
);
#8560=(
NAMED_UNIT(*)
PLANE_ANGLE_UNIT()
SI_UNIT($,.RADIAN.)
);
#8561=(
LENGTH_UNIT()
NAMED_UNIT(*)
SI_UNIT($,.METRE.)
);
#8584=PRODUCT_DEFINITION_SHAPE('','',#8599);
#8599=PRODUCT_DEFINITION('','',#8623,#8611);
#8611=PRODUCT_DEFINITION_CONTEXT('',#8674,'design');
#8623=PRODUCT_DEFINITION_FORMATION_WITH_SPECIFIED_SOURCE('','',#8647,
 .NOT_KNOWN.);
#8647=PRODUCT('CRANKSHAFT','CRANKSHAFT','CRANKSHAFT',(#8671));
#8671=PRODUCT_CONTEXT('',#8674,'mechanical');
#8674=APPLICATION_CONTEXT('managed model based 3d engineering');
ENDSEC;
END-ISO-10303-21;
